ISO-10303-21;
HEADER;
FILE_DESCRIPTION (('STEP AP214'),
    '1' );
FILE_NAME ('Servo-Body.2.step',
    '2026-11-01T06:29:40',
    ( '' ),
    ( '' ),
    'SwSTEP 2.0',
    'SolidWorks 2024',
    '' );
FILE_SCHEMA (( 'AUTOMOTIVE_DESIGN' ));
ENDSEC;

DATA;
#18=ORIENTED_EDGE ( 'NONE', *, *, #2305, .F. ) ;
#19=ADVANCED_FACE ( 'NONE', ( #19045 ), #8159, .F. ) ;
#36=VERTEX_POINT ( 'NONE', #2241 ) ;
#45=CARTESIAN_POINT ( 'NONE',  ( -18.00000000000001421, 10.00000000000000000, 36.00000000000000711 ) ) ;
#48=LINE ( 'NONE', #1353, #17512 ) ;
#63=VERTEX_POINT ( 'NONE', #6718 ) ;
#72=VERTEX_POINT ( 'NONE', #9896 ) ;
#74=LINE ( 'NONE', #11013, #15228 ) ;
#76=AXIS2_PLACEMENT_3D ( 'NONE', #6689, #11306, #1507 ) ;
#90=ORIENTED_EDGE ( 'NONE', *, *, #8211, .T. ) ;
#96=AXIS2_PLACEMENT_3D ( 'NONE', #6104, #4649, #10939 ) ;
#115=EDGE_CURVE ( 'NONE', #7815, #10453, #9998, .T. ) ;
#119=CARTESIAN_POINT ( 'NONE',  ( -36.00000000000000711, 8.000000000000000000, -19.00000000000000000 ) ) ;
#120=CYLINDRICAL_SURFACE ( 'NONE', #15953, 8.000000000000000000 ) ;
#125=DIRECTION ( 'NONE',  ( -1.156482317317881191E-15, 0.000000000000000000, -1.000000000000000000 ) ) ;
#131=DIRECTION ( 'NONE',  ( -1.000000000000000000, 0.000000000000000000, -0.000000000000000000 ) ) ;
#153=CARTESIAN_POINT ( 'NONE',  ( -31.00000000000005684, 10.00000000000000000, -23.00000000000000000 ) ) ;
#159=VERTEX_POINT ( 'NONE', #897 ) ;
#166=CARTESIAN_POINT ( 'NONE',  ( 22.99999999999998224, 0.000000000000000000, -31.00000000000003197 ) ) ;
#181=EDGE_CURVE ( 'NONE', #5834, #20212, #6394, .T. ) ;
#185=LINE ( 'NONE', #15988, #394 ) ;
#188=CARTESIAN_POINT ( 'NONE',  ( 39.99999999999999289, 0.000000000000000000, 26.00000000000000000 ) ) ;
#190=CARTESIAN_POINT ( 'NONE',  ( 31.00000000000001421, 10.00000000000000000, 22.99999999999999645 ) ) ;
#216=ADVANCED_FACE ( 'NONE', ( #1785 ), #8096, .F. ) ;
#235=ORIENTED_EDGE ( 'NONE', *, *, #11443, .F. ) ;
#238=DIRECTION ( 'NONE',  ( 0.000000000000000000, 0.000000000000000000, -1.000000000000000000 ) ) ;
#260=CARTESIAN_POINT ( 'NONE',  ( 39.99999999999999289, 10.00000000000000000, 18.99999999999999645 ) ) ;
#271=ORIENTED_EDGE ( 'NONE', *, *, #20336, .T. ) ;
#277=ADVANCED_FACE ( 'NONE', ( #7329 ), #10727, .F. ) ;
#297=ORIENTED_EDGE ( 'NONE', *, *, #12310, .T. ) ;
#301=CARTESIAN_POINT ( 'NONE',  ( 39.99999999999999289, 10.00000000000000000, 26.00000000000000000 ) ) ;
#315=ORIENTED_EDGE ( 'NONE', *, *, #6787, .F. ) ;
#326=LINE ( 'NONE', #7046, #6763 ) ;
#344=ORIENTED_EDGE ( 'NONE', *, *, #1048, .F. ) ;
#373=CARTESIAN_POINT ( 'NONE',  ( -36.00000000000000711, 8.000000000000000000, -19.00000000000000000 ) ) ;
#376=VECTOR ( 'NONE', #18670, 1000.000000000000000 ) ;
#390=ORIENTED_EDGE ( 'NONE', *, *, #839, .F. ) ;
#394=VECTOR ( 'NONE', #20369, 1000.000000000000000 ) ;
#401=LINE ( 'NONE', #9484, #887 ) ;
#408=AXIS2_PLACEMENT_3D ( 'NONE', #20132, #10776, #12527 ) ;
#433=VECTOR ( 'NONE', #12151, 1000.000000000000000 ) ;
#436=ORIENTED_EDGE ( 'NONE', *, *, #16816, .T. ) ;
#440=EDGE_CURVE ( 'NONE', #12019, #14963, #19152, .T. ) ;
#471=AXIS2_PLACEMENT_3D ( 'NONE', #16641, #10625, #2793 ) ;
#493=DIRECTION ( 'NONE',  ( -0.000000000000000000, -1.000000000000000000, -0.000000000000000000 ) ) ;
#496=CIRCLE ( 'NONE', #16324, 4.999999999999997335 ) ;
#549=EDGE_CURVE ( 'NONE', #13739, #15829, #13960, .T. ) ;
#554=EDGE_LOOP ( 'NONE', ( #11061, #4996, #7000, #1431 ) ) ;
#558=ADVANCED_FACE ( 'NONE', ( #11751 ), #3909, .T. ) ;
#572=CARTESIAN_POINT ( 'NONE',  ( -22.00000000000001776, 10.00000000000000000, 36.00000000000000711 ) ) ;
#591=CARTESIAN_POINT ( 'NONE',  ( 30.99999999999997513, 0.000000000000000000, 30.99999999999999645 ) ) ;
#593=VERTEX_POINT ( 'NONE', #981 ) ;
#597=ORIENTED_EDGE ( 'NONE', *, *, #11865, .F. ) ;
#609=LINE ( 'NONE', #12907, #9903 ) ;
#620=FACE_OUTER_BOUND ( 'NONE', #6910, .T. ) ;
#628=ADVANCED_FACE ( 'NONE', ( #17001 ), #19748, .F. ) ;
#632=DIRECTION ( 'NONE',  ( -0.000000000000000000, -1.000000000000000000, 0.000000000000000000 ) ) ;
#642=EDGE_CURVE ( 'NONE', #11944, #19482, #11992, .T. ) ;
#644=FACE_OUTER_BOUND ( 'NONE', #17782, .T. ) ;
#677=CARTESIAN_POINT ( 'NONE',  ( -26.00000000000002132, 0.000000000000000000, 40.00000000000000711 ) ) ;
#681=LINE ( 'NONE', #8232, #5072 ) ;
#694=ORIENTED_EDGE ( 'NONE', *, *, #2943, .T. ) ;
#711=ORIENTED_EDGE ( 'NONE', *, *, #816, .F. ) ;
#723=DIRECTION ( 'NONE',  ( -0.000000000000000000, -1.000000000000000000, -0.000000000000000000 ) ) ;
#729=VECTOR ( 'NONE', #9175, 1000.000000000000000 ) ;
#731=CARTESIAN_POINT ( 'NONE',  ( -40.00000000000000711, 10.00000000000000000, 26.00000000000000000 ) ) ;
#744=CARTESIAN_POINT ( 'NONE',  ( 22.99999999999998224, 10.00000000000000000, -36.99999999999999289 ) ) ;
#772=FACE_OUTER_BOUND ( 'NONE', #3860, .T. ) ;
#798=EDGE_CURVE ( 'NONE', #15238, #5834, #12871, .T. ) ;
#816=EDGE_CURVE ( 'NONE', #15238, #4974, #1821, .T. ) ;
#832=DIRECTION ( 'NONE',  ( 0.000000000000000000, 0.000000000000000000, 1.000000000000000000 ) ) ;
#839=EDGE_CURVE ( 'NONE', #19516, #19767, #11418, .T. ) ;
#842=CARTESIAN_POINT ( 'NONE',  ( -36.00000000000000711, 8.000000000000000000, -22.00000000000000355 ) ) ;
#856=DIRECTION ( 'NONE',  ( 3.854941057726246479E-16, 0.000000000000000000, -1.000000000000000000 ) ) ;
#859=EDGE_CURVE ( 'NONE', #9269, #17763, #14910, .T. ) ;
#860=DIRECTION ( 'NONE',  ( -0.000000000000000000, 1.000000000000000000, -0.000000000000000000 ) ) ;
#863=CARTESIAN_POINT ( 'NONE',  ( -31.00000000000001776, 10.00000000000000000, 31.00000000000000000 ) ) ;
#865=VERTEX_POINT ( 'NONE', #16081 ) ;
#870=PLANE ( 'NONE',  #13691 ) ;
#873=PLANE ( 'NONE',  #2277 ) ;
#887=VECTOR ( 'NONE', #4863, 1000.000000000000000 ) ;
#897=CARTESIAN_POINT ( 'NONE',  ( -40.00000000000000711, 8.000000000000000000, -26.00000000000000000 ) ) ;
#905=EDGE_CURVE ( 'NONE', #14745, #1444, #5237, .T. ) ;
#911=EDGE_LOOP ( 'NONE', ( #11381, #8892, #12685, #4970 ) ) ;
#928=ADVANCED_FACE ( 'NONE', ( #772 ), #17891, .T. ) ;
#934=LINE ( 'NONE', #13537, #8717 ) ;
#936=ORIENTED_EDGE ( 'NONE', *, *, #5252, .T. ) ;
#937=DIRECTION ( 'NONE',  ( 0.000000000000000000, 0.000000000000000000, 1.000000000000000000 ) ) ;
#941=CYLINDRICAL_SURFACE ( 'NONE', #14288, 4.000000000000007105 ) ;
#949=VECTOR ( 'NONE', #10406, 1000.000000000000000 ) ;
#950=EDGE_CURVE ( 'NONE', #6573, #15498, #5633, .T. ) ;
#955=DIRECTION ( 'NONE',  ( 0.000000000000000000, 0.000000000000000000, -1.000000000000000000 ) ) ;
#964=LINE ( 'NONE', #13573, #9811 ) ;
#981=CARTESIAN_POINT ( 'NONE',  ( 22.99999999999998224, 10.00000000000000000, 37.00000000000000711 ) ) ;
#1000=DIRECTION ( 'NONE',  ( 0.000000000000000000, -0.000000000000000000, 1.000000000000000000 ) ) ;
#1048=EDGE_CURVE ( 'NONE', #11912, #17994, #3154, .T. ) ;
#1056=DIRECTION ( 'NONE',  ( 0.000000000000000000, -0.000000000000000000, 1.000000000000000000 ) ) ;
#1078=ORIENTED_EDGE ( 'NONE', *, *, #5608, .F. ) ;
#1101=DIRECTION ( 'NONE',  ( 0.000000000000000000, 0.000000000000000000, -1.000000000000000000 ) ) ;
#1108=AXIS2_PLACEMENT_3D ( 'NONE', #5274, #19282, #17730 ) ;
#1118=CARTESIAN_POINT ( 'NONE',  ( 39.99999999999999289, 8.000000000000000000, 26.00000000000000000 ) ) ;
#1119=AXIS2_PLACEMENT_3D ( 'NONE', #10554, #15097, #13250 ) ;
#1125=ORIENTED_EDGE ( 'NONE', *, *, #2982, .F. ) ;
#1138=VECTOR ( 'NONE', #6526, 1000.000000000000000 ) ;
#1157=DIRECTION ( 'NONE',  ( -0.000000000000000000, -1.000000000000000000, -0.000000000000000000 ) ) ;
#1163=CARTESIAN_POINT ( 'NONE',  ( -22.00000000000001776, 8.000000000000000000, 33.00000000000000711 ) ) ;
#1168=DIRECTION ( 'NONE',  ( 0.000000000000000000, 1.000000000000000000, -0.000000000000000000 ) ) ;
#1187=ORIENTED_EDGE ( 'NONE', *, *, #11079, .T. ) ;
#1189=DIRECTION ( 'NONE',  ( 1.000000000000000000, 0.000000000000000000, -0.000000000000000000 ) ) ;
#1192=DIRECTION ( 'NONE',  ( 3.854941057726254367E-16, 0.000000000000000000, 1.000000000000000000 ) ) ;
#1199=ORIENTED_EDGE ( 'NONE', *, *, #16993, .F. ) ;
#1216=ORIENTED_EDGE ( 'NONE', *, *, #5858, .F. ) ;
#1217=PLANE ( 'NONE',  #8212 ) ;
#1218=FACE_OUTER_BOUND ( 'NONE', #1856, .T. ) ;
#1240=EDGE_CURVE ( 'NONE', #15834, #7815, #17674, .T. ) ;
#1243=VERTEX_POINT ( 'NONE', #14690 ) ;
#1246=FACE_OUTER_BOUND ( 'NONE', #17359, .T. ) ;
#1248=FACE_OUTER_BOUND ( 'NONE', #5306, .T. ) ;
#1250=DIRECTION ( 'NONE',  ( 3.854941057726249930E-16, 0.000000000000000000, 1.000000000000000000 ) ) ;
#1254=CARTESIAN_POINT ( 'NONE',  ( -26.00000000000002132, 10.00000000000000000, -31.00000000000003553 ) ) ;
#1259=LINE ( 'NONE', #13681, #2227 ) ;
#1265=DIRECTION ( 'NONE',  ( 0.000000000000000000, 0.000000000000000000, -1.000000000000000000 ) ) ;
#1308=LINE ( 'NONE', #17410, #7361 ) ;
#1318=CARTESIAN_POINT ( 'NONE',  ( 25.99999999999998224, 0.000000000000000000, -31.00000000000003197 ) ) ;
#1322=ORIENTED_EDGE ( 'NONE', *, *, #798, .F. ) ;
#1336=ORIENTED_EDGE ( 'NONE', *, *, #16251, .F. ) ;
#1350=VERTEX_POINT ( 'NONE', #6323 ) ;
#1353=CARTESIAN_POINT ( 'NONE',  ( -26.00000000000002132, 10.00000000000000000, 40.00000000000000711 ) ) ;
#1366=CARTESIAN_POINT ( 'NONE',  ( 31.99999999999998579, 6.000000000000000000, 22.99999999999999645 ) ) ;
#1384=EDGE_LOOP ( 'NONE', ( #4779, #18292, #1588, #8014 ) ) ;
#1389=ORIENTED_EDGE ( 'NONE', *, *, #1048, .T. ) ;
#1404=EDGE_CURVE ( 'NONE', #5330, #11398, #10849, .T. ) ;
#1405=VECTOR ( 'NONE', #7683, 1000.000000000000000 ) ;
#1406=ADVANCED_FACE ( 'NONE', ( #17129 ), #1452, .T. ) ;
#1409=ORIENTED_EDGE ( 'NONE', *, *, #9867, .T. ) ;
#1426=CARTESIAN_POINT ( 'NONE',  ( -23.00000000000002132, 10.00000000000000000, 32.00000000000000000 ) ) ;
#1427=EDGE_CURVE ( 'NONE', #6358, #14517, #1645, .T. ) ;
#1431=ORIENTED_EDGE ( 'NONE', *, *, #16993, .T. ) ;
#1432=CARTESIAN_POINT ( 'NONE',  ( 17.99999999999998224, 6.000000000000000000, -35.99999999999999289 ) ) ;
#1438=ADVANCED_FACE ( 'NONE', ( #14244 ), #120, .T. ) ;
#1443=CARTESIAN_POINT ( 'NONE',  ( 22.99999999999998224, 10.00000000000000000, 37.00000000000000711 ) ) ;
#1444=VERTEX_POINT ( 'NONE', #6635 ) ;
#1452=CYLINDRICAL_SURFACE ( 'NONE', #15626, 8.000000000000000000 ) ;
#1485=CARTESIAN_POINT ( 'NONE',  ( 22.99999999999998224, 10.00000000000000000, -31.00000000000003197 ) ) ;
#1488=DIRECTION ( 'NONE',  ( 0.000000000000000000, 0.000000000000000000, -1.000000000000000000 ) ) ;
#1498=ORIENTED_EDGE ( 'NONE', *, *, #20251, .F. ) ;
#1507=DIRECTION ( 'NONE',  ( 0.000000000000000000, -0.000000000000000000, 1.000000000000000000 ) ) ;
#1510=CARTESIAN_POINT ( 'NONE',  ( 22.99999999999998224, 10.00000000000000000, -31.00000000000003197 ) ) ;
#1511=DIRECTION ( 'NONE',  ( 1.000000000000000000, -0.000000000000000000, 0.000000000000000000 ) ) ;
#1521=DIRECTION ( 'NONE',  ( -1.000000000000000000, 0.000000000000000000, -0.000000000000000000 ) ) ;
#1527=CARTESIAN_POINT ( 'NONE',  ( 36.99999999999999289, 6.000000000000000000, 17.99999999999998934 ) ) ;
#1534=EDGE_CURVE ( 'NONE', #14088, #14515, #326, .T. ) ;
#1541=LINE ( 'NONE', #8068, #13840 ) ;
#1544=DIRECTION ( 'NONE',  ( 1.000000000000000000, 0.000000000000000000, 8.673617379884027583E-16 ) ) ;
#1561=ORIENTED_EDGE ( 'NONE', *, *, #6787, .T. ) ;
#1575=CARTESIAN_POINT ( 'NONE',  ( -22.00000000000001776, 10.00000000000000000, 33.00000000000000711 ) ) ;
#1582=CARTESIAN_POINT ( 'NONE',  ( 32.99999999999998579, 10.00000000000000000, 25.99999999999999645 ) ) ;
#1586=EDGE_CURVE ( 'NONE', #17808, #11049, #16733, .T. ) ;
#1588=ORIENTED_EDGE ( 'NONE', *, *, #8262, .F. ) ;
#1604=FACE_OUTER_BOUND ( 'NONE', #2972, .T. ) ;
#1613=ORIENTED_EDGE ( 'NONE', *, *, #19709, .F. ) ;
#1624=DIRECTION ( 'NONE',  ( -0.000000000000000000, 1.000000000000000000, -0.000000000000000000 ) ) ;
#1645=LINE ( 'NONE', #18869, #5738 ) ;
#1662=ORIENTED_EDGE ( 'NONE', *, *, #5663, .F. ) ;
#1674=DIRECTION ( 'NONE',  ( 0.000000000000000000, 0.000000000000000000, -1.000000000000000000 ) ) ;
#1687=DIRECTION ( 'NONE',  ( -1.000000000000000000, 0.000000000000000000, 0.000000000000000000 ) ) ;
#1699=DIRECTION ( 'NONE',  ( -1.000000000000000000, 0.000000000000000000, 4.956352788505159323E-16 ) ) ;
#1711=VECTOR ( 'NONE', #11232, 1000.000000000000000 ) ;
#1714=CARTESIAN_POINT ( 'NONE',  ( 25.99999999999997868, 8.000000000000000000, -39.99999999999999289 ) ) ;
#1718=DIRECTION ( 'NONE',  ( -1.000000000000000000, 0.000000000000000000, -0.000000000000000000 ) ) ;
#1738=CARTESIAN_POINT ( 'NONE',  ( -40.00000000000000711, 10.00000000000000000, -26.00000000000000000 ) ) ;
#1752=VERTEX_POINT ( 'NONE', #19034 ) ;
#1768=LINE ( 'NONE', #12417, #2588 ) ;
#1769=DIRECTION ( 'NONE',  ( 0.000000000000000000, 1.000000000000000000, 0.000000000000000000 ) ) ;
#1773=ORIENTED_EDGE ( 'NONE', *, *, #16816, .F. ) ;
#1776=VERTEX_POINT ( 'NONE', #17621 ) ;
#1785=FACE_OUTER_BOUND ( 'NONE', #13091, .T. ) ;
#1801=AXIS2_PLACEMENT_3D ( 'NONE', #6948, #7051, #4164 ) ;
#1804=LINE ( 'NONE', #15851, #18539 ) ;
#1807=AXIS2_PLACEMENT_3D ( 'NONE', #1254, #7585, #13867 ) ;
#1815=VECTOR ( 'NONE', #18990, 1000.000000000000000 ) ;
#1821=LINE ( 'NONE', #20271, #15643 ) ;
#1824=DIRECTION ( 'NONE',  ( 0.000000000000000000, 0.000000000000000000, 1.000000000000000000 ) ) ;
#1839=ORIENTED_EDGE ( 'NONE', *, *, #13826, .F. ) ;
#1846=DIRECTION ( 'NONE',  ( -0.000000000000000000, -1.000000000000000000, -0.000000000000000000 ) ) ;
#1854=CARTESIAN_POINT ( 'NONE',  ( -31.00000000000002132, 10.00000000000000000, -31.00000000000000000 ) ) ;
#1855=AXIS2_PLACEMENT_3D ( 'NONE', #16275, #9963, #7188 ) ;
#1856=EDGE_LOOP ( 'NONE', ( #6444, #17124, #18690, #18662 ) ) ;
#1859=ORIENTED_EDGE ( 'NONE', *, *, #3532, .T. ) ;
#1871=LINE ( 'NONE', #16617, #19434 ) ;
#1872=CARTESIAN_POINT ( 'NONE',  ( -31.00000000000005329, 10.00000000000000000, 26.00000000000000000 ) ) ;
#1887=CIRCLE ( 'NONE', #5217, 2.999999999999995559 ) ;
#1894=EDGE_CURVE ( 'NONE', #6891, #18687, #8370, .T. ) ;
#1909=FACE_OUTER_BOUND ( 'NONE', #18652, .T. ) ;
#1914=EDGE_CURVE ( 'NONE', #10863, #19071, #8959, .T. ) ;
#1916=DIRECTION ( 'NONE',  ( 0.000000000000000000, 1.000000000000000000, 0.000000000000000000 ) ) ;
#1921=EDGE_LOOP ( 'NONE', ( #15017, #9955, #11144, #12425 ) ) ;
#1941=EDGE_CURVE ( 'NONE', #19071, #18463, #496, .T. ) ;
#1945=AXIS2_PLACEMENT_3D ( 'NONE', #8525, #15030, #13579 ) ;
#1955=DIRECTION ( 'NONE',  ( 1.734723475976807094E-15, 0.000000000000000000, -1.000000000000000000 ) ) ;
#1959=LINE ( 'NONE', #9820, #11957 ) ;
#1966=LINE ( 'NONE', #13142, #2659 ) ;
#1976=ORIENTED_EDGE ( 'NONE', *, *, #17810, .F. ) ;
#1980=VECTOR ( 'NONE', #16805, 1000.000000000000000 ) ;
#1989=ADVANCED_FACE ( 'NONE', ( #15210 ), #16865, .F. ) ;
#1998=CARTESIAN_POINT ( 'NONE',  ( 25.99999999999997513, 10.00000000000000000, 31.00000000000003553 ) ) ;
#2007=CARTESIAN_POINT ( 'NONE',  ( -37.00000000000000711, 10.00000000000000000, 23.00000000000000000 ) ) ;
#2055=CARTESIAN_POINT ( 'NONE',  ( 18.99999999999998224, 8.000000000000000000, -39.99999999999999289 ) ) ;
#2064=DIRECTION ( 'NONE',  ( 0.000000000000000000, 0.000000000000000000, -1.000000000000000000 ) ) ;
#2072=DIRECTION ( 'NONE',  ( -0.000000000000000000, 1.000000000000000000, -0.000000000000000000 ) ) ;
#2094=VERTEX_POINT ( 'NONE', #16842 ) ;
#2111=VERTEX_POINT ( 'NONE', #4267 ) ;
#2113=STYLED_ITEM ( 'NONE', ( #10547 ), #15136 ) ;
#2126=FACE_OUTER_BOUND ( 'NONE', #9690, .T. ) ;
#2137=VECTOR ( 'NONE', #12955, 1000.000000000000000 ) ;
#2153=CARTESIAN_POINT ( 'NONE',  ( -40.00000000000000711, 10.00000000000000000, -19.00000000000000355 ) ) ;
#2170=ORIENTED_EDGE ( 'NONE', *, *, #16469, .F. ) ;
#2175=EDGE_CURVE ( 'NONE', #20182, #11766, #5911, .T. ) ;
#2176=VECTOR ( 'NONE', #6405, 1000.000000000000000 ) ;
#2226=PLANE ( 'NONE',  #1945 ) ;
#2227=VECTOR ( 'NONE', #19937, 1000.000000000000000 ) ;
#2241=CARTESIAN_POINT ( 'NONE',  ( -36.00000000000000711, 10.00000000000000000, -18.00000000000000355 ) ) ;
#2245=CARTESIAN_POINT ( 'NONE',  ( 31.99999999999998579, 6.000000000000000000, 25.99999999999999645 ) ) ;
#2264=CARTESIAN_POINT ( 'NONE',  ( -33.00000000000000000, 8.000000000000000000, -26.00000000000000355 ) ) ;
#2265=AXIS2_PLACEMENT_3D ( 'NONE', #12224, #15436, #1265 ) ;
#2277=AXIS2_PLACEMENT_3D ( 'NONE', #19428, #5336, #10077 ) ;
#2281=ORIENTED_EDGE ( 'NONE', *, *, #9691, .F. ) ;
#2288=DIRECTION ( 'NONE',  ( -1.000000000000000000, 0.000000000000000000, -3.854941057726246479E-16 ) ) ;
#2293=CARTESIAN_POINT ( 'NONE',  ( 31.00000000000001421, 0.000000000000000000, 22.99999999999999645 ) ) ;
#2295=AXIS2_PLACEMENT_3D ( 'NONE', #2468, #15920, #3542 ) ;
#2297=DIRECTION ( 'NONE',  ( 1.000000000000000000, 0.000000000000000000, 0.000000000000000000 ) ) ;
#2305=EDGE_CURVE ( 'NONE', #6700, #10453, #19184, .T. ) ;
#2309=ORIENTED_EDGE ( 'NONE', *, *, #950, .F. ) ;
#2317=ORIENTED_EDGE ( 'NONE', *, *, #7836, .T. ) ;
#2318=EDGE_CURVE ( 'NONE', #2111, #13550, #19072, .T. ) ;
#2331=AXIS2_PLACEMENT_3D ( 'NONE', #16731, #15586, #18655 ) ;
#2340=ORIENTED_EDGE ( 'NONE', *, *, #11790, .F. ) ;
#2344=AXIS2_PLACEMENT_3D ( 'NONE', #16458, #13082, #14589 ) ;
#2345=DIRECTION ( 'NONE',  ( 0.000000000000000000, 1.000000000000000000, 0.000000000000000000 ) ) ;
#2365=DIRECTION ( 'NONE',  ( -0.000000000000000000, -1.000000000000000000, 0.000000000000000000 ) ) ;
#2370=CARTESIAN_POINT ( 'NONE',  ( 18.99999999999998224, 8.000000000000000000, -39.99999999999999289 ) ) ;
#2400=FILL_AREA_STYLE_COLOUR ( '', #10666 ) ;
#2402=VECTOR ( 'NONE', #7999, 1000.000000000000000 ) ;
#2411=AXIS2_PLACEMENT_3D ( 'NONE', #15062, #3557, #17554 ) ;
#2418=VECTOR ( 'NONE', #12729, 1000.000000000000000 ) ;
#2419=VECTOR ( 'NONE', #10101, 1000.000000000000000 ) ;
#2420=AXIS2_PLACEMENT_3D ( 'NONE', #19592, #6855, #7161 ) ;
#2439=DIRECTION ( 'NONE',  ( 0.000000000000000000, 0.000000000000000000, -1.000000000000000000 ) ) ;
#2444=DIRECTION ( 'NONE',  ( -0.000000000000000000, -0.000000000000000000, -1.000000000000000000 ) ) ;
#2468=CARTESIAN_POINT ( 'NONE',  ( -36.00000000000000711, 6.000000000000000000, -22.00000000000000355 ) ) ;
#2495=CYLINDRICAL_SURFACE ( 'NONE', #14834, 3.000000000000002665 ) ;
#2496=FACE_OUTER_BOUND ( 'NONE', #10514, .T. ) ;
#2501=EDGE_CURVE ( 'NONE', #19115, #1776, #3098, .T. ) ;
#2506=ORIENTED_EDGE ( 'NONE', *, *, #4957, .T. ) ;
#2525=VECTOR ( 'NONE', #5531, 1000.000000000000000 ) ;
#2528=DIRECTION ( 'NONE',  ( 3.854941057726258312E-16, -0.000000000000000000, 1.000000000000000000 ) ) ;
#2531=CARTESIAN_POINT ( 'NONE',  ( -40.00000000000000711, 0.000000000000000000, 26.00000000000000000 ) ) ;
#2548=ORIENTED_EDGE ( 'NONE', *, *, #7945, .F. ) ;
#2571=EDGE_CURVE ( 'NONE', #20182, #10544, #7838, .T. ) ;
#2583=CARTESIAN_POINT ( 'NONE',  ( -31.00000000000007105, 0.000000000000000000, 23.00000000000000000 ) ) ;
#2588=VECTOR ( 'NONE', #20327, 1000.000000000000000 ) ;
#2594=ORIENTED_EDGE ( 'NONE', *, *, #8255, .T. ) ;
#2602=DIRECTION ( 'NONE',  ( 0.000000000000000000, 1.000000000000000000, 0.000000000000000000 ) ) ;
#2623=DIRECTION ( 'NONE',  ( -0.000000000000000000, -1.000000000000000000, -0.000000000000000000 ) ) ;
#2633=LINE ( 'NONE', #4203, #5593 ) ;
#2645=DIRECTION ( 'NONE',  ( -0.000000000000000000, 1.000000000000000000, -0.000000000000000000 ) ) ;
#2659=VECTOR ( 'NONE', #16239, 1000.000000000000000 ) ;
#2674=AXIS2_PLACEMENT_3D ( 'NONE', #8610, #20214, #15499 ) ;
#2692=ORIENTED_EDGE ( 'NONE', *, *, #12681, .T. ) ;
#2696=VERTEX_POINT ( 'NONE', #4953 ) ;
#2706=FILL_AREA_STYLE ('',( #2400 ) ) ;
#2707=EDGE_CURVE ( 'NONE', #4851, #13965, #11227, .T. ) ;
#2720=ORIENTED_EDGE ( 'NONE', *, *, #17607, .T. ) ;
#2725=VECTOR ( 'NONE', #2886, 1000.000000000000000 ) ;
#2729=CARTESIAN_POINT ( 'NONE',  ( -31.00000000000001776, 10.00000000000000000, 31.00000000000000000 ) ) ;
#2731=FACE_OUTER_BOUND ( 'NONE', #3460, .T. ) ;
#2741=AXIS2_PLACEMENT_3D ( 'NONE', #5042, #3500, #8234 ) ;
#2744=LINE ( 'NONE', #10387, #17524 ) ;
#2758=ORIENTED_EDGE ( 'NONE', *, *, #3216, .F. ) ;
#2763=DIRECTION ( 'NONE',  ( 1.000000000000000000, 0.000000000000000000, 3.854941057726246479E-16 ) ) ;
#2793=DIRECTION ( 'NONE',  ( 0.000000000000000000, 0.000000000000000000, 1.000000000000000000 ) ) ;
#2798=CYLINDRICAL_SURFACE ( 'NONE', #7716, 3.999999999999996447 ) ;
#2800=AXIS2_PLACEMENT_3D ( 'NONE', #16675, #2528, #4380 ) ;
#2819=PLANE ( 'NONE',  #8367 ) ;
#2826=ORIENTED_EDGE ( 'NONE', *, *, #5936, .F. ) ;
#2828=ORIENTED_EDGE ( 'NONE', *, *, #5623, .F. ) ;
#2865=CARTESIAN_POINT ( 'NONE',  ( 18.99999999999998224, 8.000000000000000000, -35.99999999999999289 ) ) ;
#2867=DIRECTION ( 'NONE',  ( 1.000000000000000000, 0.000000000000000000, 0.000000000000000000 ) ) ;
#2886=DIRECTION ( 'NONE',  ( -0.000000000000000000, -1.000000000000000000, -0.000000000000000000 ) ) ;
#2889=LINE ( 'NONE', #20094, #11273 ) ;
#2892=DIRECTION ( 'NONE',  ( 0.000000000000000000, 0.000000000000000000, 1.000000000000000000 ) ) ;
#2906=EDGE_CURVE ( 'NONE', #6229, #17448, #17005, .T. ) ;
#2913=ORIENTED_EDGE ( 'NONE', *, *, #3858, .F. ) ;
#2920=VERTEX_POINT ( 'NONE', #9250 ) ;
#2927=CARTESIAN_POINT ( 'NONE',  ( -23.00000000000002487, 6.000000000000000000, -36.99999999999999289 ) ) ;
#2928=CARTESIAN_POINT ( 'NONE',  ( -18.00000000000001421, 6.000000000000000000, 37.00000000000000711 ) ) ;
#2943=EDGE_CURVE ( 'NONE', #13434, #4175, #13705, .T. ) ;
#2954=ADVANCED_FACE ( 'NONE', ( #1909 ), #11109, .T. ) ;
#2964=CARTESIAN_POINT ( 'NONE',  ( -32.00000000000000711, 6.000000000000000000, -22.00000000000000355 ) ) ;
#2972=EDGE_LOOP ( 'NONE', ( #13779, #16068, #17879, #15607, #15778, #14983 ) ) ;
#2975=EDGE_CURVE ( 'NONE', #4114, #14513, #185, .T. ) ;
#2979=ORIENTED_EDGE ( 'NONE', *, *, #8936, .T. ) ;
#2980=CARTESIAN_POINT ( 'NONE',  ( -23.00000000000002132, 10.00000000000000000, 37.00000000000000711 ) ) ;
#2982=EDGE_CURVE ( 'NONE', #865, #12374, #74, .T. ) ;
#2993=LINE ( 'NONE', #13929, #5898 ) ;
#3019=CARTESIAN_POINT ( 'NONE',  ( 18.99999999999998224, 8.000000000000000000, -35.99999999999999289 ) ) ;
#3022=ORIENTED_EDGE ( 'NONE', *, *, #1404, .F. ) ;
#3025=ORIENTED_EDGE ( 'NONE', *, *, #19595, .F. ) ;
#3026=LINE ( 'NONE', #6450, #1815 ) ;
#3043=LINE ( 'NONE', #1582, #12592 ) ;
#3050=VECTOR ( 'NONE', #6748, 1000.000000000000000 ) ;
#3059=CLOSED_SHELL ( 'NONE', ( #18447, #928, #20320, #10717, #8779, #8754, #15066, #5130, #6368, #3983, #9657, #14385, #5391, #8871, #5049, #19052, #1989, #20356, #19608, #8191, #8910, #5619, #1438, #19980, #13072, #17282, #1406, #10318, #9286, #10016, #4634, #18146, #12057, #6807, #8881, #19, #6662, #3883, #13305, #6113, #19304, #10011, #14678, #6749, #11784, #14480, #16891, #15441, #15741, #19013, #15945, #6705, #628, #9238, #8277, #216, #277, #7549, #19929, #15148, #14086, #2954, #10171, #7440, #5473, #558 ) ) ;
#3075=ORIENTED_EDGE ( 'NONE', *, *, #10003, .F. ) ;
#3077=DIRECTION ( 'NONE',  ( -3.854941057726249437E-16, 0.000000000000000000, -1.000000000000000000 ) ) ;
#3078=EDGE_CURVE ( 'NONE', #17763, #6154, #19629, .T. ) ;
#3083=ORIENTED_EDGE ( 'NONE', *, *, #6477, .F. ) ;
#3098=LINE ( 'NONE', #12270, #15690 ) ;
#3112=CARTESIAN_POINT ( 'NONE',  ( 31.99999999999998579, 10.00000000000000000, 21.99999999999999645 ) ) ;
#3139=PLANE ( 'NONE',  #15282 ) ;
#3141=AXIS2_PLACEMENT_3D ( 'NONE', #15361, #10495, #1189 ) ;
#3154=LINE ( 'NONE', #2927, #1405 ) ;
#3155=DIRECTION ( 'NONE',  ( -0.000000000000000000, 1.000000000000000000, -0.000000000000000000 ) ) ;
#3157=LINE ( 'NONE', #153, #10874 ) ;
#3158=DIRECTION ( 'NONE',  ( 0.000000000000000000, 1.000000000000000000, 0.000000000000000000 ) ) ;
#3163=FACE_OUTER_BOUND ( 'NONE', #6625, .T. ) ;
#3169=PRODUCT ( 'Servo-Body.2', 'Servo-Body.2', '', ( #12612 ) ) ;
#3176=CARTESIAN_POINT ( 'NONE',  ( -26.00000000000002132, 10.00000000000000000, -39.99999999999999289 ) ) ;
#3184=DIRECTION ( 'NONE',  ( 0.000000000000000000, 0.000000000000000000, 1.000000000000000000 ) ) ;
#3188=CARTESIAN_POINT ( 'NONE',  ( -22.00000000000001776, 10.00000000000000000, 32.00000000000000711 ) ) ;
#3201=EDGE_CURVE ( 'NONE', #6154, #19577, #7194, .T. ) ;
#3208=VERTEX_POINT ( 'NONE', #6990 ) ;
#3215=ORIENTED_EDGE ( 'NONE', *, *, #14800, .T. ) ;
#3216=EDGE_CURVE ( 'NONE', #10863, #5026, #7001, .T. ) ;
#3233=CARTESIAN_POINT ( 'NONE',  ( -22.00000000000001776, 6.000000000000000000, 32.00000000000000711 ) ) ;
#3262=LINE ( 'NONE', #9644, #9583 ) ;
#3265=ORIENTED_EDGE ( 'NONE', *, *, #9487, .F. ) ;
#3267=ORIENTED_EDGE ( 'NONE', *, *, #5303, .F. ) ;
#3329=ORIENTED_EDGE ( 'NONE', *, *, #18659, .T. ) ;
#3346=ORIENTED_EDGE ( 'NONE', *, *, #16251, .T. ) ;
#3347=FACE_OUTER_BOUND ( 'NONE', #5595, .T. ) ;
#3369=VECTOR ( 'NONE', #11615, 1000.000000000000000 ) ;
#3392=CARTESIAN_POINT ( 'NONE',  ( -37.00000000000000711, 10.00000000000000000, 23.00000000000000000 ) ) ;
#3403=( GEOMETRIC_REPRESENTATION_CONTEXT ( 3 ) GLOBAL_UNCERTAINTY_ASSIGNED_CONTEXT ( ( #7010 ) ) GLOBAL_UNIT_ASSIGNED_CONTEXT ( ( #11834, #8336, #15027 ) ) REPRESENTATION_CONTEXT ( 'NONE', 'WORKASPACE' ) );
#3419=FACE_OUTER_BOUND ( 'NONE', #16911, .T. ) ;
#3436=MECHANICAL_DESIGN_GEOMETRIC_PRESENTATION_REPRESENTATION('',(#2113),#19874);
#3441=VERTEX_POINT ( 'NONE', #12747 ) ;
#3460=EDGE_LOOP ( 'NONE', ( #12134, #15489, #13261, #3083, #19207 ) ) ;
#3467=EDGE_CURVE ( 'NONE', #9680, #13739, #7338, .T. ) ;
#3483=VECTOR ( 'NONE', #2623, 1000.000000000000000 ) ;
#3493=ORIENTED_EDGE ( 'NONE', *, *, #20034, .T. ) ;
#3496=VECTOR ( 'NONE', #9893, 1000.000000000000000 ) ;
#3500=DIRECTION ( 'NONE',  ( 0.000000000000000000, 0.000000000000000000, 1.000000000000000000 ) ) ;
#3505=ORIENTED_EDGE ( 'NONE', *, *, #16960, .T. ) ;
#3506=VERTEX_POINT ( 'NONE', #9091 ) ;
#3512=ORIENTED_EDGE ( 'NONE', *, *, #3680, .F. ) ;
#3523=PLANE ( 'NONE',  #8060 ) ;
#3525=FACE_OUTER_BOUND ( 'NONE', #7407, .T. ) ;
#3527=DIRECTION ( 'NONE',  ( 0.000000000000000000, 0.000000000000000000, -1.000000000000000000 ) ) ;
#3532=EDGE_CURVE ( 'NONE', #11785, #17808, #4448, .T. ) ;
#3542=DIRECTION ( 'NONE',  ( 0.000000000000000000, 0.000000000000000000, 1.000000000000000000 ) ) ;
#3557=DIRECTION ( 'NONE',  ( 1.000000000000000000, 0.000000000000000000, 0.000000000000000000 ) ) ;
#3572=CARTESIAN_POINT ( 'NONE',  ( 22.99999999999998224, 0.000000000000000000, -31.00000000000003197 ) ) ;
#3587=EDGE_CURVE ( 'NONE', #1243, #63, #4343, .T. ) ;
#3590=CARTESIAN_POINT ( 'NONE',  ( 35.99999999999999289, 8.000000000000000000, 18.99999999999999289 ) ) ;
#3591=CARTESIAN_POINT ( 'NONE',  ( -23.00000000000002132, 10.00000000000000000, 37.00000000000000711 ) ) ;
#3604=ORIENTED_EDGE ( 'NONE', *, *, #2318, .T. ) ;
#3613=EDGE_CURVE ( 'NONE', #6600, #4111, #18549, .T. ) ;
#3660=DIRECTION ( 'NONE',  ( -0.000000000000000000, -1.000000000000000000, -0.000000000000000000 ) ) ;
#3677=VERTEX_POINT ( 'NONE', #1426 ) ;
#3680=EDGE_CURVE ( 'NONE', #10206, #9680, #7638, .T. ) ;
#3706=ORIENTED_EDGE ( 'NONE', *, *, #16349, .F. ) ;
#3730=ORIENTED_EDGE ( 'NONE', *, *, #2571, .T. ) ;
#3732=EDGE_CURVE ( 'NONE', #4111, #4175, #401, .T. ) ;
#3749=VECTOR ( 'NONE', #10153, 1000.000000000000000 ) ;
#3754=EDGE_LOOP ( 'NONE', ( #10562, #15236, #6709, #12889 ) ) ;
#3790=CARTESIAN_POINT ( 'NONE',  ( 36.99999999999999289, 10.00000000000000000, 22.99999999999999645 ) ) ;
#3797=DIRECTION ( 'NONE',  ( -0.000000000000000000, -1.000000000000000000, -0.000000000000000000 ) ) ;
#3806=ORIENTED_EDGE ( 'NONE', *, *, #16140, .T. ) ;
#3808=CARTESIAN_POINT ( 'NONE',  ( 21.99999999999998224, 10.00000000000000000, -31.99999999999998579 ) ) ;
#3815=ORIENTED_EDGE ( 'NONE', *, *, #7279, .T. ) ;
#3818=DIRECTION ( 'NONE',  ( 0.000000000000000000, 1.000000000000000000, 0.000000000000000000 ) ) ;
#3826=DIRECTION ( 'NONE',  ( 0.000000000000000000, -0.000000000000000000, 1.000000000000000000 ) ) ;
#3827=CARTESIAN_POINT ( 'NONE',  ( -32.00000000000000711, 10.00000000000000000, -22.00000000000000355 ) ) ;
#3828=FACE_OUTER_BOUND ( 'NONE', #17980, .T. ) ;
#3854=PLANE ( 'NONE',  #16117 ) ;
#3858=EDGE_CURVE ( 'NONE', #9680, #13902, #17691, .T. ) ;
#3860=EDGE_LOOP ( 'NONE', ( #15760, #15520, #4413, #16399, #14899, #12203 ) ) ;
#3876=CARTESIAN_POINT ( 'NONE',  ( -37.00000000000000711, 10.00000000000000000, 23.00000000000000000 ) ) ;
#3883=ADVANCED_FACE ( 'NONE', ( #11648 ), #17927, .F. ) ;
#3890=DIRECTION ( 'NONE',  ( -1.000000000000000000, 0.000000000000000000, 0.000000000000000000 ) ) ;
#3899=DIRECTION ( 'NONE',  ( 0.000000000000000000, 0.000000000000000000, -1.000000000000000000 ) ) ;
#3906=ORIENTED_EDGE ( 'NONE', *, *, #10622, .F. ) ;
#3909=PLANE ( 'NONE',  #16297 ) ;
#3917=FACE_OUTER_BOUND ( 'NONE', #17261, .T. ) ;
#3939=CARTESIAN_POINT ( 'NONE',  ( 17.99999999999998224, 10.00000000000000000, -35.99999999999999289 ) ) ;
#3952=EDGE_CURVE ( 'NONE', #593, #9818, #5559, .T. ) ;
#3969=EDGE_CURVE ( 'NONE', #19482, #72, #18223, .T. ) ;
#3972=CARTESIAN_POINT ( 'NONE',  ( -23.00000000000002487, 10.00000000000000000, -31.00000000000003553 ) ) ;
#3983=ADVANCED_FACE ( 'NONE', ( #12247 ), #13708, .F. ) ;
#4005=ORIENTED_EDGE ( 'NONE', *, *, #8600, .F. ) ;
#4014=FACE_OUTER_BOUND ( 'NONE', #4943, .T. ) ;
#4016=DIRECTION ( 'NONE',  ( -1.000000000000000000, 0.000000000000000000, 0.000000000000000000 ) ) ;
#4068=FACE_OUTER_BOUND ( 'NONE', #9416, .T. ) ;
#4071=LINE ( 'NONE', #5516, #12683 ) ;
#4091=DIRECTION ( 'NONE',  ( -3.854941057726253874E-16, 0.000000000000000000, -1.000000000000000000 ) ) ;
#4092=ORIENTED_EDGE ( 'NONE', *, *, #11662, .F. ) ;
#4109=CARTESIAN_POINT ( 'NONE',  ( -37.00000000000000711, 6.000000000000000000, -18.00000000000000355 ) ) ;
#4111=VERTEX_POINT ( 'NONE', #11017 ) ;
#4114=VERTEX_POINT ( 'NONE', #19259 ) ;
#4135=CARTESIAN_POINT ( 'NONE',  ( 22.99999999999998224, 10.00000000000000000, -31.00000000000003197 ) ) ;
#4139=LINE ( 'NONE', #8949, #5622 ) ;
#4142=LINE ( 'NONE', #15053, #10343 ) ;
#4154=DIRECTION ( 'NONE',  ( -1.000000000000000000, 0.000000000000000000, 0.000000000000000000 ) ) ;
#4164=DIRECTION ( 'NONE',  ( 0.000000000000000000, 0.000000000000000000, -1.000000000000000000 ) ) ;
#4175=VERTEX_POINT ( 'NONE', #188 ) ;
#4177=DIRECTION ( 'NONE',  ( 0.000000000000000000, 0.000000000000000000, 1.000000000000000000 ) ) ;
#4194=CARTESIAN_POINT ( 'NONE',  ( -40.00000000000000711, 10.00000000000000000, -26.00000000000000000 ) ) ;
#4201=CARTESIAN_POINT ( 'NONE',  ( -40.00000000000000711, 10.00000000000000000, 26.00000000000000000 ) ) ;
#4203=CARTESIAN_POINT ( 'NONE',  ( -37.00000000000000711, 10.00000000000000000, 23.00000000000000000 ) ) ;
#4231=CARTESIAN_POINT ( 'NONE',  ( 25.99999999999997868, 0.000000000000000000, -39.99999999999999289 ) ) ;
#4233=CARTESIAN_POINT ( 'NONE',  ( -26.00000000000002132, 10.00000000000000000, 40.00000000000000711 ) ) ;
#4245=PLANE ( 'NONE',  #2331 ) ;
#4252=FACE_OUTER_BOUND ( 'NONE', #9076, .T. ) ;
#4263=EDGE_CURVE ( 'NONE', #9458, #20152, #18196, .T. ) ;
#4267=CARTESIAN_POINT ( 'NONE',  ( -37.00000000000000711, 0.000000000000000000, -23.00000000000000000 ) ) ;
#4279=VECTOR ( 'NONE', #3660, 1000.000000000000000 ) ;
#4313=ORIENTED_EDGE ( 'NONE', *, *, #839, .T. ) ;
#4328=VECTOR ( 'NONE', #16695, 1000.000000000000000 ) ;
#4343=LINE ( 'NONE', #10830, #2725 ) ;
#4359=EDGE_LOOP ( 'NONE', ( #12032, #14328, #14087, #90 ) ) ;
#4374=EDGE_CURVE ( 'NONE', #20130, #8866, #1887, .T. ) ;
#4376=ORIENTED_EDGE ( 'NONE', *, *, #4957, .F. ) ;
#4380=DIRECTION ( 'NONE',  ( 1.000000000000000000, 0.000000000000000000, -3.854941057726258312E-16 ) ) ;
#4385=DIRECTION ( 'NONE',  ( -1.000000000000000000, 0.000000000000000000, 3.854941057726249930E-16 ) ) ;
#4390=VECTOR ( 'NONE', #13329, 1000.000000000000000 ) ;
#4397=CARTESIAN_POINT ( 'NONE',  ( -18.00000000000001421, 6.000000000000000000, 36.00000000000000711 ) ) ;
#4402=VECTOR ( 'NONE', #11539, 1000.000000000000000 ) ;
#4403=ORIENTED_EDGE ( 'NONE', *, *, #19626, .F. ) ;
#4413=ORIENTED_EDGE ( 'NONE', *, *, #1427, .T. ) ;
#4448=LINE ( 'NONE', #17111, #729 ) ;
#4456=EDGE_CURVE ( 'NONE', #17994, #3506, #964, .T. ) ;
#4465=CARTESIAN_POINT ( 'NONE',  ( -23.00000000000002132, 10.00000000000000000, 37.00000000000000711 ) ) ;
#4482=DIRECTION ( 'NONE',  ( 0.000000000000000000, -0.000000000000000000, 1.000000000000000000 ) ) ;
#4487=ORIENTED_EDGE ( 'NONE', *, *, #5488, .F. ) ;
#4520=ORIENTED_EDGE ( 'NONE', *, *, #11923, .T. ) ;
#4532=EDGE_CURVE ( 'NONE', #10206, #12019, #1259, .T. ) ;
#4534=DIRECTION ( 'NONE',  ( -0.000000000000000000, -1.000000000000000000, -0.000000000000000000 ) ) ;
#4554=DIRECTION ( 'NONE',  ( 0.000000000000000000, 0.000000000000000000, -1.000000000000000000 ) ) ;
#4559=FACE_BOUND ( 'NONE', #9143, .T. ) ;
#4571=CARTESIAN_POINT ( 'NONE',  ( -23.00000000000002132, 0.000000000000000000, 31.00000000000003553 ) ) ;
#4576=SHAPE_DEFINITION_REPRESENTATION ( #6303, #17354 ) ;
#4591=CARTESIAN_POINT ( 'NONE',  ( -22.00000000000001776, 8.000000000000000000, 36.00000000000000711 ) ) ;
#4599=VECTOR ( 'NONE', #19907, 1000.000000000000000 ) ;
#4626=FACE_OUTER_BOUND ( 'NONE', #14903, .T. ) ;
#4633=LINE ( 'NONE', #17195, #12832 ) ;
#4634=ADVANCED_FACE ( 'NONE', ( #9335 ), #17161, .T. ) ;
#4638=EDGE_LOOP ( 'NONE', ( #597, #11996, #15055, #6569, #16859, #10769 ) ) ;
#4642=DIRECTION ( 'NONE',  ( 0.000000000000000000, 0.000000000000000000, -1.000000000000000000 ) ) ;
#4649=DIRECTION ( 'NONE',  ( 1.000000000000000000, 0.000000000000000000, 0.000000000000000000 ) ) ;
#4656=VECTOR ( 'NONE', #14414, 1000.000000000000000 ) ;
#4674=FACE_OUTER_BOUND ( 'NONE', #4359, .T. ) ;
#4692=PLANE ( 'NONE',  #12355 ) ;
#4696=AXIS2_PLACEMENT_3D ( 'NONE', #4591, #3155, #9435 ) ;
#4700=LINE ( 'NONE', #1485, #2402 ) ;
#4708=ORIENTED_EDGE ( 'NONE', *, *, #8936, .F. ) ;
#4749=ORIENTED_EDGE ( 'NONE', *, *, #8429, .F. ) ;
#4779=ORIENTED_EDGE ( 'NONE', *, *, #15467, .T. ) ;
#4786=CARTESIAN_POINT ( 'NONE',  ( 36.99999999999999289, 10.00000000000000000, -22.99999999999999645 ) ) ;
#4813=ORIENTED_EDGE ( 'NONE', *, *, #12566, .T. ) ;
#4822=AXIS2_PLACEMENT_3D ( 'NONE', #2980, #4642, #1521 ) ;
#4832=ORIENTED_EDGE ( 'NONE', *, *, #14792, .F. ) ;
#4851=VERTEX_POINT ( 'NONE', #5712 ) ;
#4862=AXIS2_PLACEMENT_3D ( 'NONE', #10193, #19562, #3826 ) ;
#4863=DIRECTION ( 'NONE',  ( -0.000000000000000000, -1.000000000000000000, -0.000000000000000000 ) ) ;
#4879=CARTESIAN_POINT ( 'NONE',  ( 21.99999999999998224, 10.00000000000000000, -32.99999999999999289 ) ) ;
#4887=LINE ( 'NONE', #3019, #6989 ) ;
#4905=EDGE_LOOP ( 'NONE', ( #4005, #13513, #9209, #14772 ) ) ;
#4921=ORIENTED_EDGE ( 'NONE', *, *, #4263, .F. ) ;
#4929=CARTESIAN_POINT ( 'NONE',  ( 21.99999999999998224, 6.000000000000000000, -35.99999999999999289 ) ) ;
#4941=AXIS2_PLACEMENT_3D ( 'NONE', #3590, #9553, #5149 ) ;
#4943=EDGE_LOOP ( 'NONE', ( #19931, #6912, #7374, #5458, #6942, #9013 ) ) ;
#4946=ORIENTED_EDGE ( 'NONE', *, *, #4263, .T. ) ;
#4953=CARTESIAN_POINT ( 'NONE',  ( 25.99999999999997868, 10.00000000000000000, 40.00000000000000711 ) ) ;
#4955=VECTOR ( 'NONE', #14142, 1000.000000000000000 ) ;
#4957=EDGE_CURVE ( 'NONE', #12424, #19242, #1768, .T. ) ;
#4963=DIRECTION ( 'NONE',  ( 1.000000000000000000, -0.000000000000000000, 0.000000000000000000 ) ) ;
#4970=ORIENTED_EDGE ( 'NONE', *, *, #14015, .T. ) ;
#4973=VECTOR ( 'NONE', #7523, 1000.000000000000000 ) ;
#4974=VERTEX_POINT ( 'NONE', #6138 ) ;
#4989=CARTESIAN_POINT ( 'NONE',  ( 22.99999999999997513, 10.00000000000000000, 31.00000000000005684 ) ) ;
#4996=ORIENTED_EDGE ( 'NONE', *, *, #17095, .T. ) ;
#4997=ORIENTED_EDGE ( 'NONE', *, *, #13423, .F. ) ;
#5026=VERTEX_POINT ( 'NONE', #6950 ) ;
#5042=CARTESIAN_POINT ( 'NONE',  ( 0.000000000000000000, 0.000000000000000000, 0.000000000000000000 ) ) ;
#5046=PLANE ( 'NONE',  #6959 ) ;
#5049=ADVANCED_FACE ( 'NONE', ( #5201 ), #3854, .F. ) ;
#5057=ORIENTED_EDGE ( 'NONE', *, *, #642, .F. ) ;
#5061=CIRCLE ( 'NONE', #15925, 2.999999999999995559 ) ;
#5072=VECTOR ( 'NONE', #19431, 1000.000000000000000 ) ;
#5081=ORIENTED_EDGE ( 'NONE', *, *, #18566, .T. ) ;
#5092=AXIS2_PLACEMENT_3D ( 'NONE', #12155, #18428, #1101 ) ;
#5097=LINE ( 'NONE', #16042, #18437 ) ;
#5100=VERTEX_POINT ( 'NONE', #16238 ) ;
#5102=DIRECTION ( 'NONE',  ( -0.000000000000000000, -1.000000000000000000, -0.000000000000000000 ) ) ;
#5103=ORIENTED_EDGE ( 'NONE', *, *, #14065, .T. ) ;
#5108=ORIENTED_EDGE ( 'NONE', *, *, #11643, .F. ) ;
#5109=VECTOR ( 'NONE', #125, 1000.000000000000000 ) ;
#5120=VECTOR ( 'NONE', #19975, 1000.000000000000000 ) ;
#5121=DIRECTION ( 'NONE',  ( -1.000000000000000000, -0.000000000000000000, -0.000000000000000000 ) ) ;
#5130=ADVANCED_FACE ( 'NONE', ( #16930 ), #1217, .F. ) ;
#5139=VECTOR ( 'NONE', #13836, 1000.000000000000000 ) ;
#5145=ORIENTED_EDGE ( 'NONE', *, *, #13100, .T. ) ;
#5147=ORIENTED_EDGE ( 'NONE', *, *, #8164, .F. ) ;
#5149=DIRECTION ( 'NONE',  ( -1.000000000000000000, 0.000000000000000000, -8.673617379884027583E-16 ) ) ;
#5160=CARTESIAN_POINT ( 'NONE',  ( -26.00000000000001776, 8.000000000000000000, 33.00000000000000711 ) ) ;
#5182=VECTOR ( 'NONE', #4091, 1000.000000000000000 ) ;
#5186=ORIENTED_EDGE ( 'NONE', *, *, #20034, .F. ) ;
#5188=EDGE_LOOP ( 'NONE', ( #6244, #315, #16246, #11696 ) ) ;
#5200=ORIENTED_EDGE ( 'NONE', *, *, #16170, .T. ) ;
#5201=FACE_OUTER_BOUND ( 'NONE', #15260, .T. ) ;
#5207=EDGE_CURVE ( 'NONE', #18687, #11894, #9782, .T. ) ;
#5217=AXIS2_PLACEMENT_3D ( 'NONE', #5637, #6162, #10680 ) ;
#5226=EDGE_CURVE ( 'NONE', #1243, #16197, #16092, .T. ) ;
#5237=LINE ( 'NONE', #11510, #5435 ) ;
#5250=CARTESIAN_POINT ( 'NONE',  ( -19.00000000000001776, 8.000000000000000000, 40.00000000000000711 ) ) ;
#5252=EDGE_CURVE ( 'NONE', #7117, #2094, #11317, .T. ) ;
#5253=EDGE_CURVE ( 'NONE', #19516, #3677, #2993, .T. ) ;
#5263=CARTESIAN_POINT ( 'NONE',  ( 36.99999999999999289, 10.00000000000000000, 17.99999999999998934 ) ) ;
#5270=AXIS2_PLACEMENT_3D ( 'NONE', #4929, #9969, #1824 ) ;
#5274=CARTESIAN_POINT ( 'NONE',  ( 35.99999999999999289, 8.000000000000000000, 21.99999999999999645 ) ) ;
#5282=ORIENTED_EDGE ( 'NONE', *, *, #181, .F. ) ;
#5285=ORIENTED_EDGE ( 'NONE', *, *, #11923, .F. ) ;
#5294=ORIENTED_EDGE ( 'NONE', *, *, #3201, .F. ) ;
#5303=EDGE_CURVE ( 'NONE', #7139, #6891, #19383, .T. ) ;
#5306=EDGE_LOOP ( 'NONE', ( #16374, #20359, #15838, #16965 ) ) ;
#5307=DIRECTION ( 'NONE',  ( 0.000000000000000000, 1.000000000000000000, 0.000000000000000000 ) ) ;
#5330=VERTEX_POINT ( 'NONE', #1432 ) ;
#5336=DIRECTION ( 'NONE',  ( 1.000000000000000000, -0.000000000000000000, 0.000000000000000000 ) ) ;
#5344=DIRECTION ( 'NONE',  ( -0.000000000000000000, -1.000000000000000000, 0.000000000000000000 ) ) ;
#5384=CARTESIAN_POINT ( 'NONE',  ( -40.00000000000000711, 0.000000000000000000, 26.00000000000000000 ) ) ;
#5391=ADVANCED_FACE ( 'NONE', ( #17906 ), #10391, .F. ) ;
#5396=EDGE_CURVE ( 'NONE', #17052, #14513, #14803, .T. ) ;
#5414=CARTESIAN_POINT ( 'NONE',  ( -33.00000000000000000, 8.000000000000000000, -22.00000000000000355 ) ) ;
#5421=AXIS2_PLACEMENT_3D ( 'NONE', #12063, #11948, #10488 ) ;
#5435=VECTOR ( 'NONE', #9965, 1000.000000000000000 ) ;
#5449=CARTESIAN_POINT ( 'NONE',  ( 32.99999999999998579, 8.000000000000000000, 25.99999999999999645 ) ) ;
#5458=ORIENTED_EDGE ( 'NONE', *, *, #18566, .F. ) ;
#5459=EDGE_LOOP ( 'NONE', ( #12514, #1199, #3493, #5548 ) ) ;
#5467=CARTESIAN_POINT ( 'NONE',  ( -18.00000000000001421, 6.000000000000000000, 40.00000000000000711 ) ) ;
#5473=ADVANCED_FACE ( 'NONE', ( #16392 ), #2226, .F. ) ;
#5475=VECTOR ( 'NONE', #16205, 1000.000000000000000 ) ;
#5477=ORIENTED_EDGE ( 'NONE', *, *, #6739, .F. ) ;
#5479=EDGE_CURVE ( 'NONE', #19115, #9381, #18738, .T. ) ;
#5487=LINE ( 'NONE', #16221, #6954 ) ;
#5488=EDGE_CURVE ( 'NONE', #6229, #2111, #19942, .T. ) ;
#5512=DIRECTION ( 'NONE',  ( -1.000000000000000000, 0.000000000000000000, 0.000000000000000000 ) ) ;
#5516=CARTESIAN_POINT ( 'NONE',  ( -19.00000000000001776, 8.000000000000000000, 40.00000000000000711 ) ) ;
#5520=FACE_OUTER_BOUND ( 'NONE', #18029, .T. ) ;
#5531=DIRECTION ( 'NONE',  ( -0.000000000000000000, -0.000000000000000000, 1.000000000000000000 ) ) ;
#5538=CARTESIAN_POINT ( 'NONE',  ( 32.99999999999998579, 10.00000000000000000, 25.99999999999999645 ) ) ;
#5548=ORIENTED_EDGE ( 'NONE', *, *, #2175, .T. ) ;
#5559=LINE ( 'NONE', #18114, #7493 ) ;
#5572=ORIENTED_EDGE ( 'NONE', *, *, #18786, .F. ) ;
#5575=EDGE_CURVE ( 'NONE', #4974, #14996, #11846, .T. ) ;
#5579=VECTOR ( 'NONE', #7261, 1000.000000000000000 ) ;
#5593=VECTOR ( 'NONE', #10470, 1000.000000000000000 ) ;
#5595=EDGE_LOOP ( 'NONE', ( #19142, #13199, #8896, #11507 ) ) ;
#5599=DIRECTION ( 'NONE',  ( 0.000000000000000000, 1.000000000000000000, 0.000000000000000000 ) ) ;
#5601=ORIENTED_EDGE ( 'NONE', *, *, #12673, .T. ) ;
#5608=EDGE_CURVE ( 'NONE', #5100, #7117, #19693, .T. ) ;
#5619=ADVANCED_FACE ( 'NONE', ( #7170 ), #8897, .F. ) ;
#5622=VECTOR ( 'NONE', #4016, 1000.000000000000000 ) ;
#5623=EDGE_CURVE ( 'NONE', #11912, #8401, #8585, .T. ) ;
#5633=LINE ( 'NONE', #16975, #8063 ) ;
#5634=DIRECTION ( 'NONE',  ( 0.000000000000000000, 1.000000000000000000, 0.000000000000000000 ) ) ;
#5637=CARTESIAN_POINT ( 'NONE',  ( 21.99999999999998224, 8.000000000000000000, -35.99999999999999289 ) ) ;
#5646=CARTESIAN_POINT ( 'NONE',  ( 18.99999999999998224, 8.000000000000000000, -39.99999999999999289 ) ) ;
#5660=DIRECTION ( 'NONE',  ( 1.000000000000000000, 0.000000000000000000, -0.000000000000000000 ) ) ;
#5663=EDGE_CURVE ( 'NONE', #3506, #11785, #16366, .T. ) ;
#5668=VECTOR ( 'NONE', #12873, 1000.000000000000000 ) ;
#5683=CARTESIAN_POINT ( 'NONE',  ( 32.99999999999998579, 8.000000000000000000, 21.99999999999999645 ) ) ;
#5707=SURFACE_SIDE_STYLE ('',( #7263 ) ) ;
#5712=CARTESIAN_POINT ( 'NONE',  ( -31.00000000000007105, 10.00000000000000000, 23.00000000000000000 ) ) ;
#5716=EDGE_CURVE ( 'NONE', #16910, #14575, #10051, .T. ) ;
#5723=ORIENTED_EDGE ( 'NONE', *, *, #6477, .T. ) ;
#5732=FACE_OUTER_BOUND ( 'NONE', #18781, .T. ) ;
#5738=VECTOR ( 'NONE', #11152, 1000.000000000000000 ) ;
#5739=DIRECTION ( 'NONE',  ( -0.000000000000000000, -1.000000000000000000, -0.000000000000000000 ) ) ;
#5743=DIRECTION ( 'NONE',  ( 0.000000000000000000, 0.000000000000000000, -1.000000000000000000 ) ) ;
#5754=CIRCLE ( 'NONE', #5092, 7.999999999999996447 ) ;
#5758=LINE ( 'NONE', #4397, #16215 ) ;
#5760=ORIENTED_EDGE ( 'NONE', *, *, #20332, .F. ) ;
#5774=CARTESIAN_POINT ( 'NONE',  ( -37.00000000000000711, 6.000000000000000000, -23.00000000000000000 ) ) ;
#5785=DIRECTION ( 'NONE',  ( 0.000000000000000000, 0.000000000000000000, -1.000000000000000000 ) ) ;
#5794=DIRECTION ( 'NONE',  ( -0.000000000000000000, 0.000000000000000000, -1.000000000000000000 ) ) ;
#5801=CARTESIAN_POINT ( 'NONE',  ( 35.99999999999999289, 8.000000000000000000, 18.99999999999999289 ) ) ;
#5805=DIRECTION ( 'NONE',  ( 0.000000000000000000, 0.000000000000000000, 1.000000000000000000 ) ) ;
#5807=ORIENTED_EDGE ( 'NONE', *, *, #115, .T. ) ;
#5821=CARTESIAN_POINT ( 'NONE',  ( 31.00000000000001421, 10.00000000000000000, 25.99999999999999645 ) ) ;
#5834=VERTEX_POINT ( 'NONE', #15085 ) ;
#5858=EDGE_CURVE ( 'NONE', #9269, #3677, #13453, .T. ) ;
#5862=ORIENTED_EDGE ( 'NONE', *, *, #10742, .T. ) ;
#5898=VECTOR ( 'NONE', #17488, 1000.000000000000000 ) ;
#5911=LINE ( 'NONE', #18464, #5139 ) ;
#5912=PLANE ( 'NONE',  #15635 ) ;
#5913=LINE ( 'NONE', #18468, #16653 ) ;
#5936=EDGE_CURVE ( 'NONE', #6700, #5100, #18426, .T. ) ;
#5948=VECTOR ( 'NONE', #16928, 1000.000000000000000 ) ;
#5951=ORIENTED_EDGE ( 'NONE', *, *, #19058, .F. ) ;
#5955=CARTESIAN_POINT ( 'NONE',  ( -26.00000000000002132, 10.00000000000000000, -39.99999999999999289 ) ) ;
#5959=ORIENTED_EDGE ( 'NONE', *, *, #8103, .T. ) ;
#5962=CARTESIAN_POINT ( 'NONE',  ( 31.99999999999998579, 10.00000000000000000, 22.99999999999999645 ) ) ;
#5990=FACE_OUTER_BOUND ( 'NONE', #19014, .T. ) ;
#6000=DIRECTION ( 'NONE',  ( 0.000000000000000000, 0.000000000000000000, 1.000000000000000000 ) ) ;
#6004=VECTOR ( 'NONE', #6998, 1000.000000000000000 ) ;
#6018=EDGE_CURVE ( 'NONE', #15834, #6700, #13940, .T. ) ;
#6020=LINE ( 'NONE', #15510, #13482 ) ;
#6035=CARTESIAN_POINT ( 'NONE',  ( 21.99999999999998224, 8.000000000000000000, -32.99999999999999289 ) ) ;
#6036=EDGE_LOOP ( 'NONE', ( #1976, #10814, #4832, #9399, #19918, #6652, #11186, #11120, #18798, #19954, #13382, #5108, #4749, #9542, #6175, #3075 ) ) ;
#6037=VECTOR ( 'NONE', #12327, 1000.000000000000000 ) ;
#6061=ORIENTED_EDGE ( 'NONE', *, *, #11236, .T. ) ;
#6068=AXIS2_PLACEMENT_3D ( 'NONE', #8098, #20339, #6347 ) ;
#6081=LINE ( 'NONE', #12366, #8349 ) ;
#6104=CARTESIAN_POINT ( 'NONE',  ( -33.00000000000000000, 8.000000000000000000, -22.00000000000000355 ) ) ;
#6113=ADVANCED_FACE ( 'NONE', ( #11359 ), #6632, .T. ) ;
#6123=ORIENTED_EDGE ( 'NONE', *, *, #5396, .F. ) ;
#6128=DIRECTION ( 'NONE',  ( 0.000000000000000000, 1.000000000000000000, 0.000000000000000000 ) ) ;
#6138=CARTESIAN_POINT ( 'NONE',  ( 18.99999999999998224, 10.00000000000000000, -35.99999999999999289 ) ) ;
#6140=DIRECTION ( 'NONE',  ( 0.000000000000000000, 0.000000000000000000, -1.000000000000000000 ) ) ;
#6154=VERTEX_POINT ( 'NONE', #14352 ) ;
#6160=LINE ( 'NONE', #20029, #19055 ) ;
#6161=EDGE_CURVE ( 'NONE', #7486, #1776, #8274, .T. ) ;
#6162=DIRECTION ( 'NONE',  ( 0.000000000000000000, 1.000000000000000000, 0.000000000000000000 ) ) ;
#6166=PLANE ( 'NONE',  #11361 ) ;
#6175=ORIENTED_EDGE ( 'NONE', *, *, #15467, .F. ) ;
#6182=VERTEX_POINT ( 'NONE', #16225 ) ;
#6188=CARTESIAN_POINT ( 'NONE',  ( -26.00000000000002132, 0.000000000000000000, -39.99999999999999289 ) ) ;
#6205=DIRECTION ( 'NONE',  ( -1.000000000000000000, 0.000000000000000000, -0.000000000000000000 ) ) ;
#6229=VERTEX_POINT ( 'NONE', #7448 ) ;
#6235=DIRECTION ( 'NONE',  ( -0.000000000000000000, 1.000000000000000000, -0.000000000000000000 ) ) ;
#6239=EDGE_CURVE ( 'NONE', #11766, #9619, #10429, .T. ) ;
#6244=ORIENTED_EDGE ( 'NONE', *, *, #15179, .T. ) ;
#6270=ORIENTED_EDGE ( 'NONE', *, *, #6239, .F. ) ;
#6271=AXIS2_PLACEMENT_3D ( 'NONE', #16029, #1955, #17840 ) ;
#6294=ORIENTED_EDGE ( 'NONE', *, *, #6771, .T. ) ;
#6299=VECTOR ( 'NONE', #2072, 1000.000000000000000 ) ;
#6303=PRODUCT_DEFINITION_SHAPE ( 'NONE', 'NONE',  #17285 ) ;
#6306=DIRECTION ( 'NONE',  ( 0.000000000000000000, 1.000000000000000000, 0.000000000000000000 ) ) ;
#6315=ORIENTED_EDGE ( 'NONE', *, *, #4456, .T. ) ;
#6318=ORIENTED_EDGE ( 'NONE', *, *, #14800, .F. ) ;
#6323=CARTESIAN_POINT ( 'NONE',  ( -19.00000000000001776, 10.00000000000000000, 40.00000000000000711 ) ) ;
#6324=CARTESIAN_POINT ( 'NONE',  ( -31.00000000000001776, 0.000000000000000000, 31.00000000000000000 ) ) ;
#6331=DIRECTION ( 'NONE',  ( 0.000000000000000000, 0.000000000000000000, 1.000000000000000000 ) ) ;
#6347=DIRECTION ( 'NONE',  ( 0.000000000000000000, 0.000000000000000000, 1.000000000000000000 ) ) ;
#6350=ORIENTED_EDGE ( 'NONE', *, *, #1586, .T. ) ;
#6358=VERTEX_POINT ( 'NONE', #5263 ) ;
#6368=ADVANCED_FACE ( 'NONE', ( #16013 ), #9573, .F. ) ;
#6371=ORIENTED_EDGE ( 'NONE', *, *, #7836, .F. ) ;
#6373=EDGE_CURVE ( 'NONE', #11362, #16195, #14737, .T. ) ;
#6380=CARTESIAN_POINT ( 'NONE',  ( 35.99999999999999289, 6.000000000000000000, 17.99999999999998934 ) ) ;
#6388=CARTESIAN_POINT ( 'NONE',  ( -26.00000000000002132, 10.00000000000000000, 40.00000000000000711 ) ) ;
#6392=CARTESIAN_POINT ( 'NONE',  ( -37.00000000000000711, 10.00000000000000000, -18.00000000000000355 ) ) ;
#6394=LINE ( 'NONE', #9469, #4390 ) ;
#6399=ORIENTED_EDGE ( 'NONE', *, *, #2975, .F. ) ;
#6403=CIRCLE ( 'NONE', #10010, 8.000000000000000000 ) ;
#6405=DIRECTION ( 'NONE',  ( -0.000000000000000000, -1.000000000000000000, -0.000000000000000000 ) ) ;
#6433=DIRECTION ( 'NONE',  ( 0.000000000000000000, 0.000000000000000000, -1.000000000000000000 ) ) ;
#6439=ORIENTED_EDGE ( 'NONE', *, *, #1240, .F. ) ;
#6444=ORIENTED_EDGE ( 'NONE', *, *, #17693, .F. ) ;
#6450=CARTESIAN_POINT ( 'NONE',  ( 36.99999999999999289, 6.000000000000000000, 22.99999999999999645 ) ) ;
#6463=EDGE_CURVE ( 'NONE', #72, #9120, #10191, .T. ) ;
#6465=CARTESIAN_POINT ( 'NONE',  ( -26.00000000000001776, 8.000000000000000000, 33.00000000000000711 ) ) ;
#6477=EDGE_CURVE ( 'NONE', #8286, #18930, #10102, .T. ) ;
#6492=ORIENTED_EDGE ( 'NONE', *, *, #20332, .T. ) ;
#6524=DIRECTION ( 'NONE',  ( 1.000000000000000000, 0.000000000000000000, 0.000000000000000000 ) ) ;
#6525=ORIENTED_EDGE ( 'NONE', *, *, #5936, .T. ) ;
#6526=DIRECTION ( 'NONE',  ( -0.000000000000000000, 1.000000000000000000, -0.000000000000000000 ) ) ;
#6532=LINE ( 'NONE', #9506, #18339 ) ;
#6544=CARTESIAN_POINT ( 'NONE',  ( -37.00000000000000711, 10.00000000000000000, 23.00000000000000000 ) ) ;
#6569=ORIENTED_EDGE ( 'NONE', *, *, #3587, .T. ) ;
#6573=VERTEX_POINT ( 'NONE', #5962 ) ;
#6583=VECTOR ( 'NONE', #18713, 1000.000000000000000 ) ;
#6600=VERTEX_POINT ( 'NONE', #8228 ) ;
#6607=DIRECTION ( 'NONE',  ( 0.000000000000000000, 0.000000000000000000, -1.000000000000000000 ) ) ;
#6618=CARTESIAN_POINT ( 'NONE',  ( 31.00000000000003553, 0.000000000000000000, -23.00000000000000000 ) ) ;
#6625=EDGE_LOOP ( 'NONE', ( #8796, #1613, #13962, #3505 ) ) ;
#6632=PLANE ( 'NONE',  #6271 ) ;
#6635=CARTESIAN_POINT ( 'NONE',  ( 25.99999999999997513, 0.000000000000000000, 31.00000000000003553 ) ) ;
#6646=CARTESIAN_POINT ( 'NONE',  ( 21.99999999999998224, 8.000000000000000000, -32.99999999999999289 ) ) ;
#6652=ORIENTED_EDGE ( 'NONE', *, *, #6847, .F. ) ;
#6653=ORIENTED_EDGE ( 'NONE', *, *, #859, .T. ) ;
#6662=ADVANCED_FACE ( 'NONE', ( #8020 ), #17388, .T. ) ;
#6689=CARTESIAN_POINT ( 'NONE',  ( -36.00000000000000711, 8.000000000000000000, -22.00000000000000355 ) ) ;
#6694=DIRECTION ( 'NONE',  ( -1.000000000000000000, 0.000000000000000000, 0.000000000000000000 ) ) ;
#6700=VERTEX_POINT ( 'NONE', #373 ) ;
#6705=ADVANCED_FACE ( 'NONE', ( #11203 ), #16085, .F. ) ;
#6709=ORIENTED_EDGE ( 'NONE', *, *, #6373, .F. ) ;
#6710=LINE ( 'NONE', #18950, #12379 ) ;
#6715=DIRECTION ( 'NONE',  ( 0.000000000000000000, 1.000000000000000000, 0.000000000000000000 ) ) ;
#6718=CARTESIAN_POINT ( 'NONE',  ( -26.00000000000002132, 0.000000000000000000, 40.00000000000000711 ) ) ;
#6739=EDGE_CURVE ( 'NONE', #14517, #11944, #11515, .T. ) ;
#6748=DIRECTION ( 'NONE',  ( 0.000000000000000000, 1.000000000000000000, 0.000000000000000000 ) ) ;
#6749=ADVANCED_FACE ( 'NONE', ( #2126 ), #8439, .F. ) ;
#6751=VECTOR ( 'NONE', #5785, 1000.000000000000000 ) ;
#6763=VECTOR ( 'NONE', #13336, 1000.000000000000000 ) ;
#6771=EDGE_CURVE ( 'NONE', #17991, #13550, #2633, .T. ) ;
#6772=ORIENTED_EDGE ( 'NONE', *, *, #18698, .F. ) ;
#6777=CARTESIAN_POINT ( 'NONE',  ( -40.00000000000000711, 0.000000000000000000, -26.00000000000000000 ) ) ;
#6787=EDGE_CURVE ( 'NONE', #9381, #12056, #11729, .T. ) ;
#6790=LINE ( 'NONE', #1998, #12168 ) ;
#6807=ADVANCED_FACE ( 'NONE', ( #11614 ), #873, .T. ) ;
#6809=EDGE_CURVE ( 'NONE', #10453, #7117, #16160, .T. ) ;
#6822=LINE ( 'NONE', #19273, #2176 ) ;
#6824=CARTESIAN_POINT ( 'NONE',  ( 25.99999999999997868, 10.00000000000000000, 40.00000000000000711 ) ) ;
#6835=ORIENTED_EDGE ( 'NONE', *, *, #6018, .T. ) ;
#6838=ORIENTED_EDGE ( 'NONE', *, *, #17509, .F. ) ;
#6847=EDGE_CURVE ( 'NONE', #12056, #63, #19829, .T. ) ;
#6855=DIRECTION ( 'NONE',  ( -0.000000000000000000, -1.000000000000000000, 0.000000000000000000 ) ) ;
#6891=VERTEX_POINT ( 'NONE', #1163 ) ;
#6903=CARTESIAN_POINT ( 'NONE',  ( 25.99999999999997868, 10.00000000000000000, -39.99999999999999289 ) ) ;
#6910=EDGE_LOOP ( 'NONE', ( #13844, #18147, #8216, #3346 ) ) ;
#6912=ORIENTED_EDGE ( 'NONE', *, *, #7945, .T. ) ;
#6924=DIRECTION ( 'NONE',  ( 1.000000000000000000, 0.000000000000000000, 8.673617379884027583E-16 ) ) ;
#6942=ORIENTED_EDGE ( 'NONE', *, *, #6986, .F. ) ;
#6945=DIRECTION ( 'NONE',  ( 0.000000000000000000, 0.000000000000000000, -1.000000000000000000 ) ) ;
#6948=CARTESIAN_POINT ( 'NONE',  ( -37.00000000000000711, 10.00000000000000000, 23.00000000000000000 ) ) ;
#6950=CARTESIAN_POINT ( 'NONE',  ( -31.00000000000005329, 10.00000000000000000, -26.00000000000000355 ) ) ;
#6953=AXIS2_PLACEMENT_3D ( 'NONE', #863, #18283, #8816 ) ;
#6954=VECTOR ( 'NONE', #18130, 1000.000000000000000 ) ;
#6959=AXIS2_PLACEMENT_3D ( 'NONE', #3392, #9465, #1718 ) ;
#6969=CARTESIAN_POINT ( 'NONE',  ( -26.00000000000001776, 0.000000000000000000, 31.00000000000003553 ) ) ;
#6984=ORIENTED_EDGE ( 'NONE', *, *, #16087, .T. ) ;
#6986=EDGE_CURVE ( 'NONE', #7735, #15475, #3157, .T. ) ;
#6988=DIRECTION ( 'NONE',  ( -3.854941057726249437E-16, -0.000000000000000000, 1.000000000000000000 ) ) ;
#6989=VECTOR ( 'NONE', #6235, 1000.000000000000000 ) ;
#6990=CARTESIAN_POINT ( 'NONE',  ( -40.00000000000000711, 10.00000000000000000, 26.00000000000000000 ) ) ;
#6998=DIRECTION ( 'NONE',  ( -0.000000000000000000, 1.000000000000000000, -0.000000000000000000 ) ) ;
#7000=ORIENTED_EDGE ( 'NONE', *, *, #17509, .T. ) ;
#7001=CIRCLE ( 'NONE', #9288, 4.999999999999997335 ) ;
#7007=ORIENTED_EDGE ( 'NONE', *, *, #10375, .T. ) ;
#7010=UNCERTAINTY_MEASURE_WITH_UNIT (LENGTH_MEASURE( 1.000000000000000082E-05 ), #11834, 'distance_accuracy_value', 'NONE');
#7024=DIRECTION ( 'NONE',  ( 0.000000000000000000, 0.000000000000000000, 1.000000000000000000 ) ) ;
#7029=CARTESIAN_POINT ( 'NONE',  ( -23.00000000000002132, 10.00000000000000000, 31.00000000000003553 ) ) ;
#7046=CARTESIAN_POINT ( 'NONE',  ( 25.99999999999998224, 8.000000000000000000, -32.99999999999999289 ) ) ;
#7051=DIRECTION ( 'NONE',  ( 1.000000000000000000, -0.000000000000000000, 0.000000000000000000 ) ) ;
#7075=DIRECTION ( 'NONE',  ( 0.000000000000000000, 0.000000000000000000, -1.000000000000000000 ) ) ;
#7084=ORIENTED_EDGE ( 'NONE', *, *, #13423, .T. ) ;
#7091=FACE_OUTER_BOUND ( 'NONE', #6036, .T. ) ;
#7092=LINE ( 'NONE', #2531, #2525 ) ;
#7093=VECTOR ( 'NONE', #18729, 1000.000000000000000 ) ;
#7096=DIRECTION ( 'NONE',  ( 1.000000000000000000, 0.000000000000000000, 0.000000000000000000 ) ) ;
#7098=VECTOR ( 'NONE', #14759, 1000.000000000000000 ) ;
#7117=VERTEX_POINT ( 'NONE', #10100 ) ;
#7130=PLANE ( 'NONE',  #13517 ) ;
#7132=CARTESIAN_POINT ( 'NONE',  ( -26.00000000000001776, 10.00000000000000000, 33.00000000000000711 ) ) ;
#7139=VERTEX_POINT ( 'NONE', #7213 ) ;
#7161=DIRECTION ( 'NONE',  ( 0.000000000000000000, 0.000000000000000000, -1.000000000000000000 ) ) ;
#7170=FACE_OUTER_BOUND ( 'NONE', #10560, .T. ) ;
#7178=AXIS2_PLACEMENT_3D ( 'NONE', #15363, #12150, #1192 ) ;
#7187=DIRECTION ( 'NONE',  ( 0.000000000000000000, -0.000000000000000000, -1.000000000000000000 ) ) ;
#7188=DIRECTION ( 'NONE',  ( 0.000000000000000000, 0.000000000000000000, 1.000000000000000000 ) ) ;
#7193=DIRECTION ( 'NONE',  ( 0.000000000000000000, 0.000000000000000000, 1.000000000000000000 ) ) ;
#7194=LINE ( 'NONE', #16474, #3369 ) ;
#7204=LINE ( 'NONE', #5646, #10841 ) ;
#7213=CARTESIAN_POINT ( 'NONE',  ( -19.00000000000001776, 8.000000000000000000, 36.00000000000000711 ) ) ;
#7215=LINE ( 'NONE', #5774, #13308 ) ;
#7226=VECTOR ( 'NONE', #4554, 1000.000000000000000 ) ;
#7242=AXIS2_PLACEMENT_3D ( 'NONE', #591, #5344, #3899 ) ;
#7256=ORIENTED_EDGE ( 'NONE', *, *, #20216, .F. ) ;
#7261=DIRECTION ( 'NONE',  ( -0.000000000000000000, -1.000000000000000000, -0.000000000000000000 ) ) ;
#7263=SURFACE_STYLE_FILL_AREA ( #2706 ) ;
#7279=EDGE_CURVE ( 'NONE', #6573, #19318, #1541, .T. ) ;
#7291=DIRECTION ( 'NONE',  ( 0.000000000000000000, 0.000000000000000000, 1.000000000000000000 ) ) ;
#7297=DIRECTION ( 'NONE',  ( -1.000000000000000000, -0.000000000000000000, 3.854941057726258312E-16 ) ) ;
#7304=ORIENTED_EDGE ( 'NONE', *, *, #15590, .T. ) ;
#7309=CARTESIAN_POINT ( 'NONE',  ( -26.00000000000002132, 10.00000000000000000, -31.00000000000003553 ) ) ;
#7329=FACE_OUTER_BOUND ( 'NONE', #911, .T. ) ;
#7338=LINE ( 'NONE', #5801, #17203 ) ;
#7361=VECTOR ( 'NONE', #1624, 1000.000000000000000 ) ;
#7370=DIRECTION ( 'NONE',  ( 0.000000000000000000, 1.000000000000000000, 0.000000000000000000 ) ) ;
#7374=ORIENTED_EDGE ( 'NONE', *, *, #5488, .T. ) ;
#7375=CARTESIAN_POINT ( 'NONE',  ( 39.99999999999999289, 0.000000000000000000, 26.00000000000000000 ) ) ;
#7379=EDGE_CURVE ( 'NONE', #10589, #20130, #17835, .T. ) ;
#7383=AXIS2_PLACEMENT_3D ( 'NONE', #14667, #632, #14551 ) ;
#7406=CARTESIAN_POINT ( 'NONE',  ( 39.99999999999999289, 8.000000000000000000, 18.99999999999999645 ) ) ;
#7407=EDGE_LOOP ( 'NONE', ( #6492, #14730, #19998, #10254, #18668, #6399 ) ) ;
#7414=EDGE_CURVE ( 'NONE', #10365, #19318, #5487, .T. ) ;
#7426=CARTESIAN_POINT ( 'NONE',  ( -32.00000000000000711, 6.000000000000000000, -23.00000000000000000 ) ) ;
#7432=CARTESIAN_POINT ( 'NONE',  ( -22.00000000000001776, 10.00000000000000000, 32.00000000000000711 ) ) ;
#7440=ADVANCED_FACE ( 'NONE', ( #620 ), #9912, .F. ) ;
#7448=CARTESIAN_POINT ( 'NONE',  ( -37.00000000000000711, 6.000000000000000000, -23.00000000000000000 ) ) ;
#7454=CARTESIAN_POINT ( 'NONE',  ( 39.99999999999999289, 10.00000000000000000, -26.00000000000000000 ) ) ;
#7458=DIRECTION ( 'NONE',  ( 1.000000000000000000, -0.000000000000000000, 0.000000000000000000 ) ) ;
#7460=DIRECTION ( 'NONE',  ( 3.854941057726247958E-16, -0.000000000000000000, 1.000000000000000000 ) ) ;
#7463=AXIS2_PLACEMENT_3D ( 'NONE', #15156, #5307, #1000 ) ;
#7486=VERTEX_POINT ( 'NONE', #5384 ) ;
#7493=VECTOR ( 'NONE', #16612, 1000.000000000000000 ) ;
#7502=DIRECTION ( 'NONE',  ( 0.000000000000000000, 1.000000000000000000, 0.000000000000000000 ) ) ;
#7520=AXIS2_PLACEMENT_3D ( 'NONE', #19111, #17274, #9752 ) ;
#7523=DIRECTION ( 'NONE',  ( 1.000000000000000000, 0.000000000000000000, 0.000000000000000000 ) ) ;
#7548=DIRECTION ( 'NONE',  ( 0.000000000000000000, 1.000000000000000000, 0.000000000000000000 ) ) ;
#7549=ADVANCED_FACE ( 'NONE', ( #10618 ), #4245, .T. ) ;
#7557=ORIENTED_EDGE ( 'NONE', *, *, #3952, .F. ) ;
#7560=DIRECTION ( 'NONE',  ( -8.673617379884027583E-16, 0.000000000000000000, 1.000000000000000000 ) ) ;
#7585=DIRECTION ( 'NONE',  ( 1.000000000000000000, -0.000000000000000000, 3.854941057726254860E-16 ) ) ;
#7589=DIRECTION ( 'NONE',  ( 0.000000000000000000, 0.000000000000000000, 1.000000000000000000 ) ) ;
#7594=CARTESIAN_POINT ( 'NONE',  ( -40.00000000000000711, 6.000000000000000000, -18.00000000000000355 ) ) ;
#7597=ORIENTED_EDGE ( 'NONE', *, *, #3587, .F. ) ;
#7601=ORIENTED_EDGE ( 'NONE', *, *, #14957, .T. ) ;
#7602=DIRECTION ( 'NONE',  ( 0.000000000000000000, 0.000000000000000000, -1.000000000000000000 ) ) ;
#7614=LINE ( 'NONE', #7432, #433 ) ;
#7617=LINE ( 'NONE', #16717, #1980 ) ;
#7637=PLANE ( 'NONE',  #96 ) ;
#7638=LINE ( 'NONE', #9278, #11618 ) ;
#7642=AXIS2_PLACEMENT_3D ( 'NONE', #13477, #4385, #1250 ) ;
#7659=ORIENTED_EDGE ( 'NONE', *, *, #9456, .T. ) ;
#7660=CARTESIAN_POINT ( 'NONE',  ( 18.99999999999998224, 10.00000000000000000, -39.99999999999999289 ) ) ;
#7669=CARTESIAN_POINT ( 'NONE',  ( -36.00000000000000711, 6.000000000000000000, -22.00000000000000355 ) ) ;
#7683=DIRECTION ( 'NONE',  ( -1.000000000000000000, 0.000000000000000000, 0.000000000000000000 ) ) ;
#7695=CARTESIAN_POINT ( 'NONE',  ( -40.00000000000000711, 0.000000000000000000, -26.00000000000000000 ) ) ;
#7697=DIRECTION ( 'NONE',  ( -0.000000000000000000, -1.000000000000000000, 0.000000000000000000 ) ) ;
#7708=ORIENTED_EDGE ( 'NONE', *, *, #16960, .F. ) ;
#7716=AXIS2_PLACEMENT_3D ( 'NONE', #9099, #7548, #6000 ) ;
#7735=VERTEX_POINT ( 'NONE', #17319 ) ;
#7747=DIRECTION ( 'NONE',  ( -1.000000000000000000, -0.000000000000000000, -8.673617379884027583E-16 ) ) ;
#7790=VECTOR ( 'NONE', #1699, 1000.000000000000000 ) ;
#7805=CARTESIAN_POINT ( 'NONE',  ( -40.00000000000000711, 6.000000000000000000, -18.00000000000000355 ) ) ;
#7815=VERTEX_POINT ( 'NONE', #17720 ) ;
#7822=DIRECTION ( 'NONE',  ( 3.854941057726249930E-16, 0.000000000000000000, -1.000000000000000000 ) ) ;
#7827=LINE ( 'NONE', #18736, #19047 ) ;
#7836=EDGE_CURVE ( 'NONE', #11398, #3506, #17815, .T. ) ;
#7838=LINE ( 'NONE', #12698, #3496 ) ;
#7856=ORIENTED_EDGE ( 'NONE', *, *, #11643, .T. ) ;
#7862=EDGE_CURVE ( 'NONE', #2696, #14745, #16493, .T. ) ;
#7868=FACE_OUTER_BOUND ( 'NONE', #5459, .T. ) ;
#7877=VECTOR ( 'NONE', #9181, 1000.000000000000000 ) ;
#7898=CARTESIAN_POINT ( 'NONE',  ( -37.00000000000000711, 0.000000000000000000, 23.00000000000000000 ) ) ;
#7920=LINE ( 'NONE', #1714, #14590 ) ;
#7945=EDGE_CURVE ( 'NONE', #10544, #6229, #7215, .T. ) ;
#7954=EDGE_CURVE ( 'NONE', #5834, #10863, #18516, .T. ) ;
#7961=VECTOR ( 'NONE', #7096, 1000.000000000000000 ) ;
#7964=CARTESIAN_POINT ( 'NONE',  ( 22.99999999999998224, 0.000000000000000000, 37.00000000000000711 ) ) ;
#7999=DIRECTION ( 'NONE',  ( -0.000000000000000000, -1.000000000000000000, -0.000000000000000000 ) ) ;
#8014=ORIENTED_EDGE ( 'NONE', *, *, #5716, .T. ) ;
#8016=CARTESIAN_POINT ( 'NONE',  ( -23.00000000000002487, 10.00000000000000000, -36.99999999999999289 ) ) ;
#8020=FACE_OUTER_BOUND ( 'NONE', #14051, .T. ) ;
#8060=AXIS2_PLACEMENT_3D ( 'NONE', #14529, #11341, #12906 ) ;
#8062=AXIS2_PLACEMENT_3D ( 'NONE', #2729, #1157, #12210 ) ;
#8063=VECTOR ( 'NONE', #16573, 1000.000000000000000 ) ;
#8068=CARTESIAN_POINT ( 'NONE',  ( 31.99999999999998579, 10.00000000000000000, 25.99999999999999645 ) ) ;
#8085=LINE ( 'NONE', #10966, #12650 ) ;
#8096=PLANE ( 'NONE',  #2411 ) ;
#8098=CARTESIAN_POINT ( 'NONE',  ( 21.99999999999998224, 8.000000000000000000, -35.99999999999999289 ) ) ;
#8103=EDGE_CURVE ( 'NONE', #11785, #12469, #10907, .T. ) ;
#8134=DIRECTION ( 'NONE',  ( 1.000000000000000000, 0.000000000000000000, 3.854941057726246479E-16 ) ) ;
#8144=ORIENTED_EDGE ( 'NONE', *, *, #19626, .T. ) ;
#8151=ORIENTED_EDGE ( 'NONE', *, *, #11251, .T. ) ;
#8159=PLANE ( 'NONE',  #12619 ) ;
#8164=EDGE_CURVE ( 'NONE', #17991, #4851, #11419, .T. ) ;
#8178=ORIENTED_EDGE ( 'NONE', *, *, #17702, .T. ) ;
#8179=DIRECTION ( 'NONE',  ( -0.000000000000000000, -0.000000000000000000, 1.000000000000000000 ) ) ;
#8185=CARTESIAN_POINT ( 'NONE',  ( -37.00000000000000711, 10.00000000000000000, -23.00000000000000000 ) ) ;
#8191=ADVANCED_FACE ( 'NONE', ( #16574 ), #11825, .F. ) ;
#8207=EDGE_LOOP ( 'NONE', ( #18031, #4403, #17947, #5200, #7304, #10663, #16680, #16654, #8724, #8377, #8568, #16468, #19950, #8804, #15373, #711, #9077, #13401, #17547, #5103, #14395, #13653, #17886, #15598, #3806, #12209, #15442, #9697 ) ) ;
#8211=EDGE_CURVE ( 'NONE', #3208, #7486, #15327, .T. ) ;
#8212=AXIS2_PLACEMENT_3D ( 'NONE', #13443, #7460, #19680 ) ;
#8213=DIRECTION ( 'NONE',  ( 0.000000000000000000, 0.000000000000000000, 1.000000000000000000 ) ) ;
#8216=ORIENTED_EDGE ( 'NONE', *, *, #7379, .F. ) ;
#8228=CARTESIAN_POINT ( 'NONE',  ( 32.99999999999998579, 8.000000000000000000, 25.99999999999999645 ) ) ;
#8232=CARTESIAN_POINT ( 'NONE',  ( -23.00000000000002132, 10.00000000000000000, 37.00000000000000711 ) ) ;
#8234=DIRECTION ( 'NONE',  ( 1.000000000000000000, 0.000000000000000000, 0.000000000000000000 ) ) ;
#8239=VECTOR ( 'NONE', #6988, 1000.000000000000000 ) ;
#8241=VECTOR ( 'NONE', #1544, 1000.000000000000000 ) ;
#8255=EDGE_CURVE ( 'NONE', #13965, #19767, #15572, .T. ) ;
#8262=EDGE_CURVE ( 'NONE', #16910, #2920, #10950, .T. ) ;
#8264=AXIS2_PLACEMENT_3D ( 'NONE', #2055, #14854, #832 ) ;
#8274=LINE ( 'NONE', #17528, #19740 ) ;
#8277=ADVANCED_FACE ( 'NONE', ( #18700 ), #17265, .F. ) ;
#8286=VERTEX_POINT ( 'NONE', #2928 ) ;
#8287=DIRECTION ( 'NONE',  ( -0.000000000000000000, -1.000000000000000000, -0.000000000000000000 ) ) ;
#8292=ORIENTED_EDGE ( 'NONE', *, *, #2175, .F. ) ;
#8300=EDGE_CURVE ( 'NONE', #9381, #11894, #48, .T. ) ;
#8336=( NAMED_UNIT ( * ) PLANE_ANGLE_UNIT ( ) SI_UNIT ( $, .RADIAN. ) );
#8349=VECTOR ( 'NONE', #12463, 1000.000000000000000 ) ;
#8367=AXIS2_PLACEMENT_3D ( 'NONE', #9114, #7370, #4482 ) ;
#8369=VERTEX_POINT ( 'NONE', #6777 ) ;
#8370=LINE ( 'NONE', #16418, #5120 ) ;
#8377=ORIENTED_EDGE ( 'NONE', *, *, #440, .T. ) ;
#8392=EDGE_LOOP ( 'NONE', ( #3025, #15104, #1859, #6350 ) ) ;
#8401=VERTEX_POINT ( 'NONE', #17975 ) ;
#8424=LINE ( 'NONE', #12859, #14209 ) ;
#8429=EDGE_CURVE ( 'NONE', #20152, #20212, #16059, .T. ) ;
#8439=PLANE ( 'NONE',  #12848 ) ;
#8471=DIRECTION ( 'NONE',  ( 0.000000000000000000, 0.000000000000000000, 1.000000000000000000 ) ) ;
#8482=ORIENTED_EDGE ( 'NONE', *, *, #1534, .T. ) ;
#8485=EDGE_CURVE ( 'NONE', #10970, #11894, #18275, .T. ) ;
#8492=CARTESIAN_POINT ( 'NONE',  ( -23.00000000000002487, 10.00000000000000000, -36.99999999999999289 ) ) ;
#8493=ORIENTED_EDGE ( 'NONE', *, *, #14047, .T. ) ;
#8515=CARTESIAN_POINT ( 'NONE',  ( -23.00000000000002132, 10.00000000000000000, 31.00000000000003553 ) ) ;
#8525=CARTESIAN_POINT ( 'NONE',  ( 21.99999999999998224, 8.000000000000000000, -32.99999999999999289 ) ) ;
#8547=AXIS2_PLACEMENT_3D ( 'NONE', #10235, #2602, #4177 ) ;
#8550=EDGE_LOOP ( 'NONE', ( #9125, #3265, #2758, #18101 ) ) ;
#8568=ORIENTED_EDGE ( 'NONE', *, *, #19079, .T. ) ;
#8570=LINE ( 'NONE', #19681, #19534 ) ;
#8572=VECTOR ( 'NONE', #1769, 1000.000000000000000 ) ;
#8585=LINE ( 'NONE', #744, #5579 ) ;
#8589=CARTESIAN_POINT ( 'NONE',  ( 36.99999999999999289, 10.00000000000000000, -22.99999999999999645 ) ) ;
#8600=EDGE_CURVE ( 'NONE', #11049, #15475, #14199, .T. ) ;
#8606=ORIENTED_EDGE ( 'NONE', *, *, #19373, .T. ) ;
#8609=ORIENTED_EDGE ( 'NONE', *, *, #19901, .T. ) ;
#8610=CARTESIAN_POINT ( 'NONE',  ( 30.99999999999997868, 0.000000000000000000, -30.99999999999999645 ) ) ;
#8643=DIRECTION ( 'NONE',  ( 0.000000000000000000, -0.000000000000000000, 1.000000000000000000 ) ) ;
#8659=CARTESIAN_POINT ( 'NONE',  ( -19.00000000000001776, 10.00000000000000000, 40.00000000000000711 ) ) ;
#8682=DIRECTION ( 'NONE',  ( 1.000000000000000000, 0.000000000000000000, 0.000000000000000000 ) ) ;
#8687=CARTESIAN_POINT ( 'NONE',  ( 35.99999999999999289, 10.00000000000000000, 17.99999999999998934 ) ) ;
#8695=ORIENTED_EDGE ( 'NONE', *, *, #5253, .F. ) ;
#8707=CARTESIAN_POINT ( 'NONE',  ( -22.00000000000001776, 10.00000000000000000, 33.00000000000000711 ) ) ;
#8708=FACE_OUTER_BOUND ( 'NONE', #11634, .T. ) ;
#8717=VECTOR ( 'NONE', #19793, 1000.000000000000000 ) ;
#8724=ORIENTED_EDGE ( 'NONE', *, *, #10742, .F. ) ;
#8743=DIRECTION ( 'NONE',  ( -1.000000000000000000, 0.000000000000000000, -0.000000000000000000 ) ) ;
#8750=EDGE_CURVE ( 'NONE', #593, #19577, #16466, .T. ) ;
#8752=AXIS2_PLACEMENT_3D ( 'NONE', #9215, #8825, #8916 ) ;
#8754=ADVANCED_FACE ( 'NONE', ( #7091, #10161 ), #13384, .T. ) ;
#8757=ORIENTED_EDGE ( 'NONE', *, *, #11779, .F. ) ;
#8771=LINE ( 'NONE', #12934, #8572 ) ;
#8774=PLANE ( 'NONE',  #15634 ) ;
#8779=ADVANCED_FACE ( 'NONE', ( #10261, #4559 ), #870, .F. ) ;
#8782=ORIENTED_EDGE ( 'NONE', *, *, #17693, .T. ) ;
#8791=CIRCLE ( 'NONE', #1855, 3.999999999999996447 ) ;
#8796=ORIENTED_EDGE ( 'NONE', *, *, #13100, .F. ) ;
#8802=CARTESIAN_POINT ( 'NONE',  ( 31.99999999999998579, 6.000000000000000000, 21.99999999999999645 ) ) ;
#8804=ORIENTED_EDGE ( 'NONE', *, *, #11251, .F. ) ;
#8816=DIRECTION ( 'NONE',  ( 0.000000000000000000, 0.000000000000000000, -1.000000000000000000 ) ) ;
#8820=DIRECTION ( 'NONE',  ( 0.000000000000000000, 0.000000000000000000, -1.000000000000000000 ) ) ;
#8825=DIRECTION ( 'NONE',  ( 1.000000000000000000, -0.000000000000000000, 0.000000000000000000 ) ) ;
#8866=VERTEX_POINT ( 'NONE', #6035 ) ;
#8871=ADVANCED_FACE ( 'NONE', ( #5732 ), #12314, .F. ) ;
#8879=DIRECTION ( 'NONE',  ( -0.000000000000000000, 1.000000000000000000, -0.000000000000000000 ) ) ;
#8881=ADVANCED_FACE ( 'NONE', ( #1246 ), #10770, .F. ) ;
#8884=PLANE ( 'NONE',  #12991 ) ;
#8892=ORIENTED_EDGE ( 'NONE', *, *, #5207, .F. ) ;
#8896=ORIENTED_EDGE ( 'NONE', *, *, #4374, .F. ) ;
#8897=PLANE ( 'NONE',  #20030 ) ;
#8900=VECTOR ( 'NONE', #1511, 1000.000000000000000 ) ;
#8910=ADVANCED_FACE ( 'NONE', ( #18181 ), #11919, .F. ) ;
#8911=ORIENTED_EDGE ( 'NONE', *, *, #3613, .F. ) ;
#8916=DIRECTION ( 'NONE',  ( 0.000000000000000000, 0.000000000000000000, -1.000000000000000000 ) ) ;
#8936=EDGE_CURVE ( 'NONE', #159, #8369, #15418, .T. ) ;
#8949=CARTESIAN_POINT ( 'NONE',  ( 25.99999999999998224, 6.000000000000000000, -31.99999999999998579 ) ) ;
#8959=LINE ( 'NONE', #13514, #16648 ) ;
#8992=VECTOR ( 'NONE', #9461, 1000.000000000000000 ) ;
#9005=DIRECTION ( 'NONE',  ( 0.000000000000000000, 0.000000000000000000, 1.000000000000000000 ) ) ;
#9013=ORIENTED_EDGE ( 'NONE', *, *, #10881, .T. ) ;
#9024=AXIS2_PLACEMENT_3D ( 'NONE', #17919, #3818, #10099 ) ;
#9044=LINE ( 'NONE', #15231, #18407 ) ;
#9046=EDGE_CURVE ( 'NONE', #6182, #14021, #3026, .T. ) ;
#9052=CIRCLE ( 'NONE', #1119, 4.000000000000007105 ) ;
#9053=PLANE ( 'NONE',  #14044 ) ;
#9076=EDGE_LOOP ( 'NONE', ( #4092, #15628, #5723, #15288 ) ) ;
#9077=ORIENTED_EDGE ( 'NONE', *, *, #798, .T. ) ;
#9091=CARTESIAN_POINT ( 'NONE',  ( 17.99999999999998224, 10.00000000000000000, -36.99999999999999289 ) ) ;
#9092=CARTESIAN_POINT ( 'NONE',  ( 21.99999999999998224, 10.00000000000000000, -32.99999999999999289 ) ) ;
#9099=CARTESIAN_POINT ( 'NONE',  ( -22.00000000000001776, 6.000000000000000000, 36.00000000000000711 ) ) ;
#9114=CARTESIAN_POINT ( 'NONE',  ( -36.00000000000000711, 6.000000000000000000, -22.00000000000000355 ) ) ;
#9120=VERTEX_POINT ( 'NONE', #18895 ) ;
#9125=ORIENTED_EDGE ( 'NONE', *, *, #1941, .T. ) ;
#9126=CARTESIAN_POINT ( 'NONE',  ( -22.00000000000001776, 6.000000000000000000, 36.00000000000000711 ) ) ;
#9127=ORIENTED_EDGE ( 'NONE', *, *, #15557, .F. ) ;
#9132=FACE_OUTER_BOUND ( 'NONE', #12575, .T. ) ;
#9136=CARTESIAN_POINT ( 'NONE',  ( 25.99999999999997513, 10.00000000000000000, 31.00000000000003553 ) ) ;
#9143=EDGE_LOOP ( 'NONE', ( #9709, #8609, #11560, #16725, #9944, #10069, #20121, #1662, #6371, #13583, #5572, #14714, #5057, #5477, #12161, #13362, #18337, #10160, #5760, #5951, #7557, #15098, #20186, #8782, #17307, #8695, #1773, #5147 ) ) ;
#9157=FACE_OUTER_BOUND ( 'NONE', #11122, .T. ) ;
#9163=EDGE_LOOP ( 'NONE', ( #1322, #1336, #11408, #4946, #18991, #5282 ) ) ;
#9175=DIRECTION ( 'NONE',  ( -0.000000000000000000, -0.000000000000000000, 1.000000000000000000 ) ) ;
#9181=DIRECTION ( 'NONE',  ( 1.000000000000000000, 0.000000000000000000, 0.000000000000000000 ) ) ;
#9203=CARTESIAN_POINT ( 'NONE',  ( -18.00000000000001421, 6.000000000000000000, 36.00000000000000711 ) ) ;
#9209=ORIENTED_EDGE ( 'NONE', *, *, #19571, .T. ) ;
#9215=CARTESIAN_POINT ( 'NONE',  ( 17.99999999999998224, 6.000000000000000000, -35.99999999999999289 ) ) ;
#9222=EDGE_CURVE ( 'NONE', #10544, #9619, #17670, .T. ) ;
#9231=FACE_OUTER_BOUND ( 'NONE', #554, .T. ) ;
#9232=DIRECTION ( 'NONE',  ( -0.000000000000000000, -0.000000000000000000, 1.000000000000000000 ) ) ;
#9233=CARTESIAN_POINT ( 'NONE',  ( -37.00000000000000711, 10.00000000000000000, -23.00000000000000000 ) ) ;
#9238=ADVANCED_FACE ( 'NONE', ( #644 ), #19308, .T. ) ;
#9239=VERTEX_POINT ( 'NONE', #10047 ) ;
#9247=ORIENTED_EDGE ( 'NONE', *, *, #14957, .F. ) ;
#9250=CARTESIAN_POINT ( 'NONE',  ( 25.99999999999998224, 10.00000000000000000, -31.00000000000003197 ) ) ;
#9252=CARTESIAN_POINT ( 'NONE',  ( 31.99999999999998579, 6.000000000000000000, 25.99999999999999645 ) ) ;
#9269=VERTEX_POINT ( 'NONE', #14113 ) ;
#9278=CARTESIAN_POINT ( 'NONE',  ( 35.99999999999999289, 8.000000000000000000, 18.99999999999999289 ) ) ;
#9286=ADVANCED_FACE ( 'NONE', ( #12476 ), #19979, .T. ) ;
#9288=AXIS2_PLACEMENT_3D ( 'NONE', #19724, #20136, #5743 ) ;
#9312=VECTOR ( 'NONE', #7297, 1000.000000000000000 ) ;
#9316=ORIENTED_EDGE ( 'NONE', *, *, #11779, .T. ) ;
#9335=FACE_OUTER_BOUND ( 'NONE', #15346, .T. ) ;
#9354=ORIENTED_EDGE ( 'NONE', *, *, #5396, .T. ) ;
#9363=LINE ( 'NONE', #12459, #7093 ) ;
#9369=VECTOR ( 'NONE', #10074, 1000.000000000000000 ) ;
#9370=FACE_OUTER_BOUND ( 'NONE', #18814, .T. ) ;
#9381=VERTEX_POINT ( 'NONE', #11038 ) ;
#9396=LINE ( 'NONE', #20200, #1711 ) ;
#9399=ORIENTED_EDGE ( 'NONE', *, *, #905, .F. ) ;
#9400=CARTESIAN_POINT ( 'NONE',  ( -40.00000000000000711, 8.000000000000000000, -19.00000000000000355 ) ) ;
#9404=ORIENTED_EDGE ( 'NONE', *, *, #17057, .F. ) ;
#9407=EDGE_LOOP ( 'NONE', ( #8151, #12133, #5285, #17939 ) ) ;
#9416=EDGE_LOOP ( 'NONE', ( #20012, #4376, #7601, #12547 ) ) ;
#9424=ORIENTED_EDGE ( 'NONE', *, *, #2906, .F. ) ;
#9435=DIRECTION ( 'NONE',  ( 0.000000000000000000, 0.000000000000000000, 1.000000000000000000 ) ) ;
#9443=PLANE ( 'NONE',  #16553 ) ;
#9452=CARTESIAN_POINT ( 'NONE',  ( -31.00000000000002132, 0.000000000000000000, -31.00000000000000000 ) ) ;
#9456=EDGE_CURVE ( 'NONE', #19242, #6358, #6710, .T. ) ;
#9458=VERTEX_POINT ( 'NONE', #14632 ) ;
#9461=DIRECTION ( 'NONE',  ( 1.000000000000000000, 0.000000000000000000, 0.000000000000000000 ) ) ;
#9463=DIRECTION ( 'NONE',  ( -0.000000000000000000, -1.000000000000000000, -0.000000000000000000 ) ) ;
#9465=DIRECTION ( 'NONE',  ( 0.000000000000000000, 0.000000000000000000, -1.000000000000000000 ) ) ;
#9469=CARTESIAN_POINT ( 'NONE',  ( -26.00000000000002132, 10.00000000000000000, -39.99999999999999289 ) ) ;
#9472=ORIENTED_EDGE ( 'NONE', *, *, #7862, .T. ) ;
#9484=CARTESIAN_POINT ( 'NONE',  ( 39.99999999999999289, 10.00000000000000000, 26.00000000000000000 ) ) ;
#9487=EDGE_CURVE ( 'NONE', #5026, #18463, #6822, .T. ) ;
#9499=ORIENTED_EDGE ( 'NONE', *, *, #14065, .F. ) ;
#9501=CARTESIAN_POINT ( 'NONE',  ( -31.00000000000001776, 10.00000000000000000, 31.00000000000000000 ) ) ;
#9506=CARTESIAN_POINT ( 'NONE',  ( 36.99999999999999289, 0.000000000000000000, 22.99999999999999645 ) ) ;
#9542=ORIENTED_EDGE ( 'NONE', *, *, #19373, .F. ) ;
#9548=CARTESIAN_POINT ( 'NONE',  ( -33.00000000000000000, 8.000000000000000000, -26.00000000000000355 ) ) ;
#9552=ORIENTED_EDGE ( 'NONE', *, *, #18691, .T. ) ;
#9553=DIRECTION ( 'NONE',  ( 8.673617379884027583E-16, 0.000000000000000000, -1.000000000000000000 ) ) ;
#9559=LINE ( 'NONE', #17395, #14989 ) ;
#9573=CYLINDRICAL_SURFACE ( 'NONE', #14466, 5.000000000000000888 ) ;
#9579=CARTESIAN_POINT ( 'NONE',  ( -26.00000000000002132, 0.000000000000000000, -31.00000000000003553 ) ) ;
#9583=VECTOR ( 'NONE', #19006, 1000.000000000000000 ) ;
#9597=DIRECTION ( 'NONE',  ( 1.000000000000000000, 0.000000000000000000, 0.000000000000000000 ) ) ;
#9598=LINE ( 'NONE', #4786, #4955 ) ;
#9603=DIRECTION ( 'NONE',  ( 1.000000000000000000, 0.000000000000000000, 0.000000000000000000 ) ) ;
#9619=VERTEX_POINT ( 'NONE', #10904 ) ;
#9621=CYLINDRICAL_SURFACE ( 'NONE', #6068, 2.999999999999995559 ) ;
#9644=CARTESIAN_POINT ( 'NONE',  ( 31.00000000000001421, 6.000000000000000000, 22.99999999999999645 ) ) ;
#9657=ADVANCED_FACE ( 'NONE', ( #16894 ), #9053, .F. ) ;
#9680=VERTEX_POINT ( 'NONE', #11415 ) ;
#9690=EDGE_LOOP ( 'NONE', ( #9404, #16093, #2506, #7659 ) ) ;
#9691=EDGE_CURVE ( 'NONE', #18923, #159, #14397, .T. ) ;
#9697=ORIENTED_EDGE ( 'NONE', *, *, #8485, .F. ) ;
#9709=ORIENTED_EDGE ( 'NONE', *, *, #18922, .F. ) ;
#9731=CARTESIAN_POINT ( 'NONE',  ( 17.99999999999998579, 6.000000000000000000, -36.99999999999999289 ) ) ;
#9742=VECTOR ( 'NONE', #16248, 1000.000000000000000 ) ;
#9752=DIRECTION ( 'NONE',  ( 0.000000000000000000, 0.000000000000000000, -1.000000000000000000 ) ) ;
#9763=EDGE_LOOP ( 'NONE', ( #12095, #2170, #17883, #9472 ) ) ;
#9775=VECTOR ( 'NONE', #15421, 1000.000000000000000 ) ;
#9782=LINE ( 'NONE', #5160, #12140 ) ;
#9805=CARTESIAN_POINT ( 'NONE',  ( 32.99999999999998579, 10.00000000000000000, 21.99999999999999645 ) ) ;
#9811=VECTOR ( 'NONE', #1168, 1000.000000000000000 ) ;
#9818=VERTEX_POINT ( 'NONE', #19518 ) ;
#9820=CARTESIAN_POINT ( 'NONE',  ( 22.99999999999998224, 6.000000000000000000, -31.00000000000003197 ) ) ;
#9856=ORIENTED_EDGE ( 'NONE', *, *, #12566, .F. ) ;
#9867=EDGE_CURVE ( 'NONE', #8369, #7486, #7092, .T. ) ;
#9874=ADVANCED_BREP_SHAPE_REPRESENTATION ( '', ( #15136, #2741 ), #3403 ) ;
#9880=EDGE_CURVE ( 'NONE', #18930, #19948, #8791, .T. ) ;
#9890=EDGE_CURVE ( 'NONE', #2920, #14515, #15016, .T. ) ;
#9893=DIRECTION ( 'NONE',  ( 0.000000000000000000, 0.000000000000000000, -1.000000000000000000 ) ) ;
#9896=CARTESIAN_POINT ( 'NONE',  ( 22.99999999999998224, 10.00000000000000000, -31.99999999999998579 ) ) ;
#9903=VECTOR ( 'NONE', #11650, 1000.000000000000000 ) ;
#9912=PLANE ( 'NONE',  #8264 ) ;
#9943=CARTESIAN_POINT ( 'NONE',  ( 31.00000000000001776, 10.00000000000000000, -25.99999999999999645 ) ) ;
#9944=ORIENTED_EDGE ( 'NONE', *, *, #10881, .F. ) ;
#9955=ORIENTED_EDGE ( 'NONE', *, *, #16087, .F. ) ;
#9958=DIRECTION ( 'NONE',  ( -0.000000000000000000, -1.000000000000000000, -0.000000000000000000 ) ) ;
#9959=ORIENTED_EDGE ( 'NONE', *, *, #19666, .T. ) ;
#9961=ORIENTED_EDGE ( 'NONE', *, *, #14193, .T. ) ;
#9963=DIRECTION ( 'NONE',  ( 0.000000000000000000, 1.000000000000000000, 0.000000000000000000 ) ) ;
#9965=DIRECTION ( 'NONE',  ( -3.854941057726249437E-16, 0.000000000000000000, -1.000000000000000000 ) ) ;
#9969=DIRECTION ( 'NONE',  ( 0.000000000000000000, 1.000000000000000000, 0.000000000000000000 ) ) ;
#9976=SHAPE_REPRESENTATION_RELATIONSHIP ( 'NONE' , 'NONE' ,  #17354, #9874 ) ;
#9996=CARTESIAN_POINT ( 'NONE',  ( 30.99999999999997868, 10.00000000000000000, -30.99999999999999645 ) ) ;
#9998=LINE ( 'NONE', #2153, #19510 ) ;
#10003=EDGE_CURVE ( 'NONE', #9239, #14575, #13672, .T. ) ;
#10010=AXIS2_PLACEMENT_3D ( 'NONE', #12509, #14061, #6140 ) ;
#10011=ADVANCED_FACE ( 'NONE', ( #2731 ), #15211, .F. ) ;
#10016=ADVANCED_FACE ( 'NONE', ( #1248 ), #20021, .T. ) ;
#10047=CARTESIAN_POINT ( 'NONE',  ( 39.99999999999999289, 0.000000000000000000, -26.00000000000000000 ) ) ;
#10051=LINE ( 'NONE', #9943, #4279 ) ;
#10059=ORIENTED_EDGE ( 'NONE', *, *, #5716, .F. ) ;
#10064=DIRECTION ( 'NONE',  ( 0.000000000000000000, 1.000000000000000000, 0.000000000000000000 ) ) ;
#10069=ORIENTED_EDGE ( 'NONE', *, *, #19571, .F. ) ;
#10074=DIRECTION ( 'NONE',  ( -0.000000000000000000, -1.000000000000000000, -0.000000000000000000 ) ) ;
#10077=DIRECTION ( 'NONE',  ( 0.000000000000000000, 0.000000000000000000, -1.000000000000000000 ) ) ;
#10085=LINE ( 'NONE', #5449, #6004 ) ;
#10099=DIRECTION ( 'NONE',  ( 0.000000000000000000, 0.000000000000000000, 1.000000000000000000 ) ) ;
#10100=CARTESIAN_POINT ( 'NONE',  ( -33.00000000000000000, 10.00000000000000000, -22.00000000000000355 ) ) ;
#10101=DIRECTION ( 'NONE',  ( 0.000000000000000000, 0.000000000000000000, -1.000000000000000000 ) ) ;
#10102=LINE ( 'NONE', #5467, #11168 ) ;
#10105=CARTESIAN_POINT ( 'NONE',  ( 35.99999999999999289, 8.000000000000000000, 21.99999999999999645 ) ) ;
#10110=VERTEX_POINT ( 'NONE', #45 ) ;
#10113=UNCERTAINTY_MEASURE_WITH_UNIT (LENGTH_MEASURE( 1.000000000000000082E-05 ), #18578, 'distance_accuracy_value', 'NONE');
#10126=CARTESIAN_POINT ( 'NONE',  ( -19.00000000000001776, 8.000000000000000000, 40.00000000000000711 ) ) ;
#10149=ORIENTED_EDGE ( 'NONE', *, *, #181, .T. ) ;
#10153=DIRECTION ( 'NONE',  ( -0.000000000000000000, -0.000000000000000000, 1.000000000000000000 ) ) ;
#10160=ORIENTED_EDGE ( 'NONE', *, *, #7279, .F. ) ;
#10161=FACE_BOUND ( 'NONE', #12297, .T. ) ;
#10164=DIRECTION ( 'NONE',  ( 0.000000000000000000, 0.000000000000000000, 1.000000000000000000 ) ) ;
#10171=ADVANCED_FACE ( 'NONE', ( #3347 ), #9621, .F. ) ;
#10180=EDGE_LOOP ( 'NONE', ( #16837, #18045, #9247, #2692, #10773 ) ) ;
#10191=LINE ( 'NONE', #11754, #949 ) ;
#10193=CARTESIAN_POINT ( 'NONE',  ( 21.99999999999998224, 6.000000000000000000, -35.99999999999999289 ) ) ;
#10205=ORIENTED_EDGE ( 'NONE', *, *, #19068, .T. ) ;
#10206=VERTEX_POINT ( 'NONE', #18056 ) ;
#10222=DIRECTION ( 'NONE',  ( 1.000000000000000000, -0.000000000000000000, 0.000000000000000000 ) ) ;
#10223=DIRECTION ( 'NONE',  ( -1.000000000000000000, -0.000000000000000000, -0.000000000000000000 ) ) ;
#10235=CARTESIAN_POINT ( 'NONE',  ( -36.00000000000000711, 8.000000000000000000, -22.00000000000000355 ) ) ;
#10254=ORIENTED_EDGE ( 'NONE', *, *, #13166, .T. ) ;
#10256=AXIS2_PLACEMENT_3D ( 'NONE', #9452, #19011, #7602 ) ;
#10261=FACE_OUTER_BOUND ( 'NONE', #8207, .T. ) ;
#10267=DIRECTION ( 'NONE',  ( -0.000000000000000000, -1.000000000000000000, -0.000000000000000000 ) ) ;
#10276=DIRECTION ( 'NONE',  ( -0.000000000000000000, -1.000000000000000000, -0.000000000000000000 ) ) ;
#10300=CIRCLE ( 'NONE', #16571, 4.000000000000003553 ) ;
#10306=CARTESIAN_POINT ( 'NONE',  ( -26.00000000000002132, 10.00000000000000000, 40.00000000000000711 ) ) ;
#10311=DIRECTION ( 'NONE',  ( -0.000000000000000000, -1.000000000000000000, -0.000000000000000000 ) ) ;
#10318=ADVANCED_FACE ( 'NONE', ( #13939 ), #12097, .T. ) ;
#10343=VECTOR ( 'NONE', #13511, 1000.000000000000000 ) ;
#10362=CIRCLE ( 'NONE', #18252, 5.000000000000000888 ) ;
#10365=VERTEX_POINT ( 'NONE', #8802 ) ;
#10375=EDGE_CURVE ( 'NONE', #19767, #6154, #934, .T. ) ;
#10377=CARTESIAN_POINT ( 'NONE',  ( -36.00000000000000711, 10.00000000000000000, -22.00000000000000355 ) ) ;
#10383=CARTESIAN_POINT ( 'NONE',  ( 35.99999999999999289, 6.000000000000000000, 17.99999999999998934 ) ) ;
#10387=CARTESIAN_POINT ( 'NONE',  ( -37.00000000000000711, 0.000000000000000000, -23.00000000000000000 ) ) ;
#10391=CYLINDRICAL_SURFACE ( 'NONE', #10843, 4.999999999999997335 ) ;
#10402=DIRECTION ( 'NONE',  ( -0.000000000000000000, 0.000000000000000000, 1.000000000000000000 ) ) ;
#10406=DIRECTION ( 'NONE',  ( 0.000000000000000000, -1.000000000000000000, 0.000000000000000000 ) ) ;
#10413=LINE ( 'NONE', #4233, #4973 ) ;
#10416=DIRECTION ( 'NONE',  ( -1.000000000000000000, 0.000000000000000000, -0.000000000000000000 ) ) ;
#10429=LINE ( 'NONE', #13723, #14447 ) ;
#10453=VERTEX_POINT ( 'NONE', #10846 ) ;
#10461=LINE ( 'NONE', #7375, #10606 ) ;
#10470=DIRECTION ( 'NONE',  ( -0.000000000000000000, -1.000000000000000000, -0.000000000000000000 ) ) ;
#10474=CARTESIAN_POINT ( 'NONE',  ( 36.99999999999999289, 0.000000000000000000, 22.99999999999999645 ) ) ;
#10488=DIRECTION ( 'NONE',  ( 0.000000000000000000, 0.000000000000000000, -1.000000000000000000 ) ) ;
#10495=DIRECTION ( 'NONE',  ( 0.000000000000000000, 0.000000000000000000, 1.000000000000000000 ) ) ;
#10505=VECTOR ( 'NONE', #6715, 1000.000000000000000 ) ;
#10514=EDGE_LOOP ( 'NONE', ( #17641, #18518, #6294, #15082, #4487, #10697 ) ) ;
#10526=VECTOR ( 'NONE', #17559, 1000.000000000000000 ) ;
#10528=DIRECTION ( 'NONE',  ( -0.000000000000000000, 1.000000000000000000, -0.000000000000000000 ) ) ;
#10532=PLANE ( 'NONE',  #11941 ) ;
#10544=VERTEX_POINT ( 'NONE', #7426 ) ;
#10547=PRESENTATION_STYLE_ASSIGNMENT (( #10645 ) ) ;
#10553=CIRCLE ( 'NONE', #2295, 4.000000000000000000 ) ;
#10554=CARTESIAN_POINT ( 'NONE',  ( 35.99999999999999289, 10.00000000000000000, 21.99999999999999645 ) ) ;
#10558=DIRECTION ( 'NONE',  ( 0.000000000000000000, 1.000000000000000000, 0.000000000000000000 ) ) ;
#10560=EDGE_LOOP ( 'NONE', ( #8911, #7084, #1125, #6984, #694, #18891 ) ) ;
#10562=ORIENTED_EDGE ( 'NONE', *, *, #6463, .F. ) ;
#10589=VERTEX_POINT ( 'NONE', #12361 ) ;
#10606=VECTOR ( 'NONE', #8820, 1000.000000000000000 ) ;
#10618=FACE_OUTER_BOUND ( 'NONE', #15233, .T. ) ;
#10622=EDGE_CURVE ( 'NONE', #15498, #10365, #20059, .T. ) ;
#10625=DIRECTION ( 'NONE',  ( 0.000000000000000000, 1.000000000000000000, 0.000000000000000000 ) ) ;
#10645=SURFACE_STYLE_USAGE ( .BOTH. , #5707 ) ;
#10648=DIRECTION ( 'NONE',  ( -0.000000000000000000, 1.000000000000000000, -0.000000000000000000 ) ) ;
#10659=ORIENTED_EDGE ( 'NONE', *, *, #5858, .T. ) ;
#10660=AXIS2_PLACEMENT_3D ( 'NONE', #9126, #13759, #1056 ) ;
#10663=ORIENTED_EDGE ( 'NONE', *, *, #2982, .T. ) ;
#10666=COLOUR_RGB ( '', 0.40784314, 0.44705882, 0.49803922) ;
#10680=DIRECTION ( 'NONE',  ( 0.000000000000000000, 0.000000000000000000, 1.000000000000000000 ) ) ;
#10697=ORIENTED_EDGE ( 'NONE', *, *, #2906, .T. ) ;
#10699=DIRECTION ( 'NONE',  ( 1.000000000000000000, 0.000000000000000000, -0.000000000000000000 ) ) ;
#10705=ORIENTED_EDGE ( 'NONE', *, *, #3467, .T. ) ;
#10717=ADVANCED_FACE ( 'NONE', ( #9157 ), #18326, .T. ) ;
#10727=PLANE ( 'NONE',  #18530 ) ;
#10733=DIRECTION ( 'NONE',  ( 1.000000000000000000, -0.000000000000000000, 4.956352788505159323E-16 ) ) ;
#10742=EDGE_CURVE ( 'NONE', #12019, #13739, #9363, .T. ) ;
#10769=ORIENTED_EDGE ( 'NONE', *, *, #7862, .F. ) ;
#10770=PLANE ( 'NONE',  #8752 ) ;
#10773=ORIENTED_EDGE ( 'NONE', *, *, #9046, .F. ) ;
#10776=DIRECTION ( 'NONE',  ( -0.000000000000000000, -1.000000000000000000, 0.000000000000000000 ) ) ;
#10814=ORIENTED_EDGE ( 'NONE', *, *, #2943, .F. ) ;
#10830=CARTESIAN_POINT ( 'NONE',  ( -26.00000000000002132, 10.00000000000000000, 40.00000000000000711 ) ) ;
#10841=VECTOR ( 'NONE', #2645, 1000.000000000000000 ) ;
#10843=AXIS2_PLACEMENT_3D ( 'NONE', #17803, #10276, #15125 ) ;
#10844=CARTESIAN_POINT ( 'NONE',  ( 30.99999999999997868, 10.00000000000000000, -30.99999999999999645 ) ) ;
#10846=CARTESIAN_POINT ( 'NONE',  ( -36.00000000000000711, 10.00000000000000000, -19.00000000000000000 ) ) ;
#10849=LINE ( 'NONE', #20223, #17568 ) ;
#10860=VECTOR ( 'NONE', #2444, 1000.000000000000000 ) ;
#10863=VERTEX_POINT ( 'NONE', #15217 ) ;
#10874=VECTOR ( 'NONE', #14268, 1000.000000000000000 ) ;
#10881=EDGE_CURVE ( 'NONE', #7735, #9619, #6160, .T. ) ;
#10904=CARTESIAN_POINT ( 'NONE',  ( -32.00000000000000711, 10.00000000000000000, -23.00000000000000000 ) ) ;
#10907=LINE ( 'NONE', #8016, #5668 ) ;
#10922=APPLICATION_CONTEXT ( 'automotive_design' ) ;
#10925=ORIENTED_EDGE ( 'NONE', *, *, #13826, .T. ) ;
#10932=ORIENTED_EDGE ( 'NONE', *, *, #3201, .T. ) ;
#10938=ORIENTED_EDGE ( 'NONE', *, *, #17810, .T. ) ;
#10939=DIRECTION ( 'NONE',  ( 0.000000000000000000, 0.000000000000000000, -1.000000000000000000 ) ) ;
#10950=CIRCLE ( 'NONE', #408, 5.000000000000000888 ) ;
#10966=CARTESIAN_POINT ( 'NONE',  ( 31.00000000000001776, 10.00000000000000000, -25.99999999999999645 ) ) ;
#10970=VERTEX_POINT ( 'NONE', #1575 ) ;
#11013=CARTESIAN_POINT ( 'NONE',  ( 31.00000000000001421, 10.00000000000000000, 25.99999999999999645 ) ) ;
#11017=CARTESIAN_POINT ( 'NONE',  ( 39.99999999999999289, 8.000000000000000000, 26.00000000000000000 ) ) ;
#11038=CARTESIAN_POINT ( 'NONE',  ( -26.00000000000001776, 10.00000000000000000, 31.00000000000003553 ) ) ;
#11048=CIRCLE ( 'NONE', #7383, 5.000000000000000888 ) ;
#11049=VERTEX_POINT ( 'NONE', #11905 ) ;
#11061=ORIENTED_EDGE ( 'NONE', *, *, #19901, .F. ) ;
#11079=EDGE_CURVE ( 'NONE', #5330, #17994, #6020, .T. ) ;
#11083=ORIENTED_EDGE ( 'NONE', *, *, #14193, .F. ) ;
#11087=CARTESIAN_POINT ( 'NONE',  ( 35.99999999999999289, 6.000000000000000000, 21.99999999999999645 ) ) ;
#11109=PLANE ( 'NONE',  #76 ) ;
#11114=CARTESIAN_POINT ( 'NONE',  ( -23.00000000000002132, 6.000000000000000000, 37.00000000000000711 ) ) ;
#11120=ORIENTED_EDGE ( 'NONE', *, *, #6161, .F. ) ;
#11122=EDGE_LOOP ( 'NONE', ( #1389, #6315, #19305, #5959, #9127, #2828 ) ) ;
#11144=ORIENTED_EDGE ( 'NONE', *, *, #15590, .F. ) ;
#11149=CARTESIAN_POINT ( 'NONE',  ( -40.00000000000000711, 8.000000000000000000, -19.00000000000000355 ) ) ;
#11152=DIRECTION ( 'NONE',  ( 0.000000000000000000, 0.000000000000000000, -1.000000000000000000 ) ) ;
#11161=CARTESIAN_POINT ( 'NONE',  ( -40.00000000000000711, 10.00000000000000000, 26.00000000000000000 ) ) ;
#11168=VECTOR ( 'NONE', #19959, 1000.000000000000000 ) ;
#11184=VECTOR ( 'NONE', #5599, 1000.000000000000000 ) ;
#11186=ORIENTED_EDGE ( 'NONE', *, *, #15179, .F. ) ;
#11203=FACE_OUTER_BOUND ( 'NONE', #14392, .T. ) ;
#11211=VECTOR ( 'NONE', #14206, 1000.000000000000000 ) ;
#11227=LINE ( 'NONE', #16016, #5475 ) ;
#11232=DIRECTION ( 'NONE',  ( 0.000000000000000000, 0.000000000000000000, -1.000000000000000000 ) ) ;
#11234=ORIENTED_EDGE ( 'NONE', *, *, #3613, .T. ) ;
#11236=EDGE_CURVE ( 'NONE', #12416, #20017, #6532, .T. ) ;
#11241=ORIENTED_EDGE ( 'NONE', *, *, #6373, .T. ) ;
#11251=EDGE_CURVE ( 'NONE', #14996, #14515, #15618, .T. ) ;
#11252=VECTOR ( 'NONE', #5739, 1000.000000000000000 ) ;
#11260=DIRECTION ( 'NONE',  ( -0.000000000000000000, -1.000000000000000000, -0.000000000000000000 ) ) ;
#11266=ORIENTED_EDGE ( 'NONE', *, *, #5226, .T. ) ;
#11273=VECTOR ( 'NONE', #17028, 1000.000000000000000 ) ;
#11306=DIRECTION ( 'NONE',  ( 0.000000000000000000, 1.000000000000000000, 0.000000000000000000 ) ) ;
#11317=LINE ( 'NONE', #11524, #7226 ) ;
#11339=VECTOR ( 'NONE', #18722, 1000.000000000000000 ) ;
#11341=DIRECTION ( 'NONE',  ( -1.000000000000000000, 0.000000000000000000, 0.000000000000000000 ) ) ;
#11342=PLANE ( 'NONE',  #14498 ) ;
#11359=FACE_OUTER_BOUND ( 'NONE', #15815, .T. ) ;
#11361=AXIS2_PLACEMENT_3D ( 'NONE', #7805, #18500, #13873 ) ;
#11362=VERTEX_POINT ( 'NONE', #12927 ) ;
#11381=ORIENTED_EDGE ( 'NONE', *, *, #8485, .T. ) ;
#11398=VERTEX_POINT ( 'NONE', #3939 ) ;
#11408=ORIENTED_EDGE ( 'NONE', *, *, #20336, .F. ) ;
#11415=CARTESIAN_POINT ( 'NONE',  ( 35.99999999999999289, 8.000000000000000000, 18.99999999999999289 ) ) ;
#11418=LINE ( 'NONE', #8515, #9369 ) ;
#11419=LINE ( 'NONE', #2007, #7961 ) ;
#11443=EDGE_CURVE ( 'NONE', #14963, #9239, #2889, .T. ) ;
#11449=DIRECTION ( 'NONE',  ( 0.000000000000000000, 0.000000000000000000, -1.000000000000000000 ) ) ;
#11472=DIRECTION ( 'NONE',  ( 0.000000000000000000, 0.000000000000000000, -1.000000000000000000 ) ) ;
#11493=ORIENTED_EDGE ( 'NONE', *, *, #13636, .T. ) ;
#11507=ORIENTED_EDGE ( 'NONE', *, *, #17936, .T. ) ;
#11510=CARTESIAN_POINT ( 'NONE',  ( 25.99999999999997868, 0.000000000000000000, 40.00000000000000711 ) ) ;
#11515=LINE ( 'NONE', #17795, #14801 ) ;
#11524=CARTESIAN_POINT ( 'NONE',  ( -33.00000000000000000, 10.00000000000000000, -22.00000000000000355 ) ) ;
#11539=DIRECTION ( 'NONE',  ( -0.000000000000000000, -1.000000000000000000, -0.000000000000000000 ) ) ;
#11560=ORIENTED_EDGE ( 'NONE', *, *, #18999, .T. ) ;
#11604=VECTOR ( 'NONE', #18962, 1000.000000000000000 ) ;
#11614=FACE_OUTER_BOUND ( 'NONE', #8392, .T. ) ;
#11615=DIRECTION ( 'NONE',  ( 1.000000000000000000, 0.000000000000000000, 0.000000000000000000 ) ) ;
#11618=VECTOR ( 'NONE', #7747, 1000.000000000000000 ) ;
#11631=ORIENTED_EDGE ( 'NONE', *, *, #10003, .T. ) ;
#11634=EDGE_LOOP ( 'NONE', ( #5807, #18, #19347, #18271 ) ) ;
#11643=EDGE_CURVE ( 'NONE', #20212, #19071, #15596, .T. ) ;
#11648=FACE_OUTER_BOUND ( 'NONE', #19324, .T. ) ;
#11650=DIRECTION ( 'NONE',  ( -4.956352788505164254E-16, 0.000000000000000000, 1.000000000000000000 ) ) ;
#11662=EDGE_CURVE ( 'NONE', #3441, #10110, #9396, .T. ) ;
#11666=AXIS2_PLACEMENT_3D ( 'NONE', #18320, #16706, #10402 ) ;
#11674=CIRCLE ( 'NONE', #13639, 8.000000000000000000 ) ;
#11696=ORIENTED_EDGE ( 'NONE', *, *, #2501, .T. ) ;
#11729=LINE ( 'NONE', #13277, #17107 ) ;
#11746=VERTEX_POINT ( 'NONE', #6618 ) ;
#11751=FACE_OUTER_BOUND ( 'NONE', #20316, .T. ) ;
#11754=CARTESIAN_POINT ( 'NONE',  ( 22.99999999999998224, 10.00000000000000000, -31.99999999999998579 ) ) ;
#11766=VERTEX_POINT ( 'NONE', #3827 ) ;
#11779=EDGE_CURVE ( 'NONE', #18687, #1243, #609, .T. ) ;
#11782=CARTESIAN_POINT ( 'NONE',  ( -40.00000000000000711, 10.00000000000000000, -18.00000000000000355 ) ) ;
#11784=ADVANCED_FACE ( 'NONE', ( #3917 ), #11342, .F. ) ;
#11785=VERTEX_POINT ( 'NONE', #16212 ) ;
#11790=EDGE_CURVE ( 'NONE', #13550, #13965, #17727, .T. ) ;
#11792=ORIENTED_EDGE ( 'NONE', *, *, #7954, .F. ) ;
#11797=CARTESIAN_POINT ( 'NONE',  ( -23.00000000000002132, 10.00000000000000000, 32.00000000000000711 ) ) ;
#11799=CARTESIAN_POINT ( 'NONE',  ( 21.99999999999998224, 10.00000000000000000, -35.99999999999999289 ) ) ;
#11816=EDGE_CURVE ( 'NONE', #9120, #11362, #4139, .T. ) ;
#11825=PLANE ( 'NONE',  #7642 ) ;
#11834=( LENGTH_UNIT ( ) NAMED_UNIT ( * ) SI_UNIT ( .MILLI., .METRE. ) );
#11846=CIRCLE ( 'NONE', #16457, 2.999999999999995559 ) ;
#11864=DIRECTION ( 'NONE',  ( 0.000000000000000000, 0.000000000000000000, -1.000000000000000000 ) ) ;
#11865=EDGE_CURVE ( 'NONE', #1350, #2696, #10413, .T. ) ;
#11894=VERTEX_POINT ( 'NONE', #7132 ) ;
#11895=VECTOR ( 'NONE', #2867, 1000.000000000000000 ) ;
#11905=CARTESIAN_POINT ( 'NONE',  ( -23.00000000000002842, 0.000000000000000000, -31.00000000000003553 ) ) ;
#11906=LINE ( 'NONE', #18163, #19254 ) ;
#11912=VERTEX_POINT ( 'NONE', #13507 ) ;
#11919=CYLINDRICAL_SURFACE ( 'NONE', #12365, 5.000000000000000888 ) ;
#11923=EDGE_CURVE ( 'NONE', #8866, #14088, #19112, .T. ) ;
#11941=AXIS2_PLACEMENT_3D ( 'NONE', #16830, #7458, #14012 ) ;
#11944=VERTEX_POINT ( 'NONE', #13895 ) ;
#11948=DIRECTION ( 'NONE',  ( -0.000000000000000000, -1.000000000000000000, 0.000000000000000000 ) ) ;
#11957=VECTOR ( 'NONE', #2064, 1000.000000000000000 ) ;
#11964=AXIS2_PLACEMENT_3D ( 'NONE', #6388, #12776, #7822 ) ;
#11966=CARTESIAN_POINT ( 'NONE',  ( -31.00000000000002132, 0.000000000000000000, -31.00000000000000000 ) ) ;
#11967=VERTEX_POINT ( 'NONE', #3572 ) ;
#11992=CIRCLE ( 'NONE', #5421, 7.999999999999996447 ) ;
#11996=ORIENTED_EDGE ( 'NONE', *, *, #12673, .F. ) ;
#12016=FACE_OUTER_BOUND ( 'NONE', #17529, .T. ) ;
#12019=VERTEX_POINT ( 'NONE', #260 ) ;
#12032=ORIENTED_EDGE ( 'NONE', *, *, #6161, .T. ) ;
#12038=DIRECTION ( 'NONE',  ( 1.000000000000000000, 0.000000000000000000, -0.000000000000000000 ) ) ;
#12056=VERTEX_POINT ( 'NONE', #6969 ) ;
#12057=ADVANCED_FACE ( 'NONE', ( #5520 ), #19504, .T. ) ;
#12063=CARTESIAN_POINT ( 'NONE',  ( 30.99999999999997868, 10.00000000000000000, -30.99999999999999645 ) ) ;
#12095=ORIENTED_EDGE ( 'NONE', *, *, #905, .T. ) ;
#12097=PLANE ( 'NONE',  #17268 ) ;
#12116=CARTESIAN_POINT ( 'NONE',  ( 31.00000000000001776, 0.000000000000000000, -25.99999999999999645 ) ) ;
#12133=ORIENTED_EDGE ( 'NONE', *, *, #1534, .F. ) ;
#12134=ORIENTED_EDGE ( 'NONE', *, *, #859, .F. ) ;
#12140=VECTOR ( 'NONE', #14618, 1000.000000000000000 ) ;
#12141=DIRECTION ( 'NONE',  ( -1.000000000000000000, 0.000000000000000000, 0.000000000000000000 ) ) ;
#12150=DIRECTION ( 'NONE',  ( -1.000000000000000000, 0.000000000000000000, 3.854941057726254367E-16 ) ) ;
#12151=DIRECTION ( 'NONE',  ( -1.000000000000000000, 0.000000000000000000, -1.734723475976807094E-15 ) ) ;
#12155=CARTESIAN_POINT ( 'NONE',  ( 30.99999999999997868, 0.000000000000000000, -30.99999999999999645 ) ) ;
#12161=ORIENTED_EDGE ( 'NONE', *, *, #1427, .F. ) ;
#12168=VECTOR ( 'NONE', #9958, 1000.000000000000000 ) ;
#12189=VECTOR ( 'NONE', #11260, 1000.000000000000000 ) ;
#12192=DIRECTION ( 'NONE',  ( 0.000000000000000000, 0.000000000000000000, -1.000000000000000000 ) ) ;
#12203=ORIENTED_EDGE ( 'NONE', *, *, #13166, .F. ) ;
#12209=ORIENTED_EDGE ( 'NONE', *, *, #5479, .T. ) ;
#12210=DIRECTION ( 'NONE',  ( 0.000000000000000000, 0.000000000000000000, -1.000000000000000000 ) ) ;
#12224=CARTESIAN_POINT ( 'NONE',  ( -31.00000000000001776, 10.00000000000000000, 31.00000000000000000 ) ) ;
#12227=DIRECTION ( 'NONE',  ( 0.000000000000000000, 0.000000000000000000, -1.000000000000000000 ) ) ;
#12247=FACE_OUTER_BOUND ( 'NONE', #20019, .T. ) ;
#12268=VECTOR ( 'NONE', #14756, 1000.000000000000000 ) ;
#12270=CARTESIAN_POINT ( 'NONE',  ( -31.00000000000005329, 10.00000000000000000, 26.00000000000000000 ) ) ;
#12292=( NAMED_UNIT ( * ) PLANE_ANGLE_UNIT ( ) SI_UNIT ( $, .RADIAN. ) );
#12297=EDGE_LOOP ( 'NONE', ( #15523, #14475, #5081, #3604, #13221, #2594, #7007, #10932, #9959, #9354, #18078, #6061, #5145, #20221, #11493, #18537 ) ) ;
#12310=EDGE_CURVE ( 'NONE', #3441, #593, #681, .T. ) ;
#12314=PLANE ( 'NONE',  #2800 ) ;
#12322=DIRECTION ( 'NONE',  ( -0.000000000000000000, -1.000000000000000000, 0.000000000000000000 ) ) ;
#12327=DIRECTION ( 'NONE',  ( -0.000000000000000000, 1.000000000000000000, -0.000000000000000000 ) ) ;
#12336=CARTESIAN_POINT ( 'NONE',  ( 30.99999999999997868, 0.000000000000000000, -30.99999999999999645 ) ) ;
#12346=ORIENTED_EDGE ( 'NONE', *, *, #9222, .T. ) ;
#12355=AXIS2_PLACEMENT_3D ( 'NONE', #11087, #3158, #14170 ) ;
#12361=CARTESIAN_POINT ( 'NONE',  ( 18.99999999999998224, 8.000000000000000000, -39.99999999999999289 ) ) ;
#12365=AXIS2_PLACEMENT_3D ( 'NONE', #15107, #16770, #955 ) ;
#12366=CARTESIAN_POINT ( 'NONE',  ( 32.99999999999998579, 8.000000000000000000, 25.99999999999999645 ) ) ;
#12374=VERTEX_POINT ( 'NONE', #5538 ) ;
#12379=VECTOR ( 'NONE', #17717, 1000.000000000000000 ) ;
#12387=CARTESIAN_POINT ( 'NONE',  ( 25.99999999999998224, 8.000000000000000000, -32.99999999999999289 ) ) ;
#12409=DIRECTION ( 'NONE',  ( -0.000000000000000000, -1.000000000000000000, -0.000000000000000000 ) ) ;
#12410=DIRECTION ( 'NONE',  ( 0.000000000000000000, 0.000000000000000000, -1.000000000000000000 ) ) ;
#12416=VERTEX_POINT ( 'NONE', #10474 ) ;
#12417=CARTESIAN_POINT ( 'NONE',  ( 35.99999999999999289, 6.000000000000000000, 17.99999999999998934 ) ) ;
#12418=CARTESIAN_POINT ( 'NONE',  ( 31.00000000000001776, 10.00000000000000000, -25.99999999999999645 ) ) ;
#12424=VERTEX_POINT ( 'NONE', #10383 ) ;
#12425=ORIENTED_EDGE ( 'NONE', *, *, #16469, .T. ) ;
#12458=CARTESIAN_POINT ( 'NONE',  ( 31.00000000000001421, 0.000000000000000000, 25.99999999999999645 ) ) ;
#12459=CARTESIAN_POINT ( 'NONE',  ( 35.99999999999999289, 10.00000000000000000, 18.99999999999999289 ) ) ;
#12463=DIRECTION ( 'NONE',  ( -0.000000000000000000, -0.000000000000000000, 1.000000000000000000 ) ) ;
#12469=VERTEX_POINT ( 'NONE', #17070 ) ;
#12476=FACE_OUTER_BOUND ( 'NONE', #14016, .T. ) ;
#12491=DIRECTION ( 'NONE',  ( -3.854941057726253874E-16, 0.000000000000000000, -1.000000000000000000 ) ) ;
#12492=ORIENTED_EDGE ( 'NONE', *, *, #19058, .T. ) ;
#12509=CARTESIAN_POINT ( 'NONE',  ( 30.99999999999997513, 10.00000000000000000, 30.99999999999999645 ) ) ;
#12514=ORIENTED_EDGE ( 'NONE', *, *, #18999, .F. ) ;
#12516=LINE ( 'NONE', #17252, #14872 ) ;
#12527=DIRECTION ( 'NONE',  ( 0.000000000000000000, 0.000000000000000000, -1.000000000000000000 ) ) ;
#12547=ORIENTED_EDGE ( 'NONE', *, *, #7414, .T. ) ;
#12552=DIRECTION ( 'NONE',  ( 0.000000000000000000, 0.000000000000000000, 1.000000000000000000 ) ) ;
#12566=EDGE_CURVE ( 'NONE', #159, #15834, #17569, .T. ) ;
#12575=EDGE_LOOP ( 'NONE', ( #7856, #16812, #11792, #10149 ) ) ;
#12590=VECTOR ( 'NONE', #3797, 1000.000000000000000 ) ;
#12592=VECTOR ( 'NONE', #9232, 1000.000000000000000 ) ;
#12595=DIRECTION ( 'NONE',  ( 0.000000000000000000, 0.000000000000000000, -1.000000000000000000 ) ) ;
#12612=PRODUCT_CONTEXT ( 'NONE', #13053, 'mechanical' ) ;
#12619=AXIS2_PLACEMENT_3D ( 'NONE', #15892, #18847, #6205 ) ;
#12628=ORIENTED_EDGE ( 'NONE', *, *, #2571, .F. ) ;
#12645=CARTESIAN_POINT ( 'NONE',  ( -31.00000000000005684, 0.000000000000000000, -23.00000000000000000 ) ) ;
#12650=VECTOR ( 'NONE', #14364, 1000.000000000000000 ) ;
#12673=EDGE_CURVE ( 'NONE', #16197, #1350, #4071, .T. ) ;
#12676=AXIS2_PLACEMENT_3D ( 'NONE', #3790, #3890, #10164 ) ;
#12681=EDGE_CURVE ( 'NONE', #12424, #14021, #11906, .T. ) ;
#12683=VECTOR ( 'NONE', #860, 1000.000000000000000 ) ;
#12685=ORIENTED_EDGE ( 'NONE', *, *, #1894, .F. ) ;
#12698=CARTESIAN_POINT ( 'NONE',  ( -32.00000000000000711, 6.000000000000000000, -22.00000000000000355 ) ) ;
#12710=EDGE_CURVE ( 'NONE', #19242, #19318, #9052, .T. ) ;
#12729=DIRECTION ( 'NONE',  ( -1.000000000000000000, 0.000000000000000000, -1.734723475976807094E-15 ) ) ;
#12747=CARTESIAN_POINT ( 'NONE',  ( -18.00000000000001421, 10.00000000000000000, 37.00000000000000711 ) ) ;
#12761=VECTOR ( 'NONE', #15142, 1000.000000000000000 ) ;
#12776=DIRECTION ( 'NONE',  ( 1.000000000000000000, -0.000000000000000000, 3.854941057726249930E-16 ) ) ;
#12826=CARTESIAN_POINT ( 'NONE',  ( 22.99999999999997513, 0.000000000000000000, 31.00000000000005684 ) ) ;
#12832=VECTOR ( 'NONE', #3077, 1000.000000000000000 ) ;
#12848=AXIS2_PLACEMENT_3D ( 'NONE', #6380, #7193, #12038 ) ;
#12851=CARTESIAN_POINT ( 'NONE',  ( -40.00000000000000711, 8.000000000000000000, -26.00000000000000000 ) ) ;
#12859=CARTESIAN_POINT ( 'NONE',  ( 25.99999999999998224, 8.000000000000000000, -32.99999999999999289 ) ) ;
#12870=EDGE_LOOP ( 'NONE', ( #1216, #6653, #20245, #17915, #390, #18265 ) ) ;
#12871=LINE ( 'NONE', #3176, #11339 ) ;
#12873=DIRECTION ( 'NONE',  ( -0.000000000000000000, -1.000000000000000000, -0.000000000000000000 ) ) ;
#12889=ORIENTED_EDGE ( 'NONE', *, *, #11816, .F. ) ;
#12903=EDGE_LOOP ( 'NONE', ( #18900, #4997, #1498, #15314 ) ) ;
#12906=DIRECTION ( 'NONE',  ( 0.000000000000000000, 0.000000000000000000, 1.000000000000000000 ) ) ;
#12907=CARTESIAN_POINT ( 'NONE',  ( -26.00000000000001776, 8.000000000000000000, 33.00000000000000711 ) ) ;
#12927=CARTESIAN_POINT ( 'NONE',  ( 21.99999999999998224, 6.000000000000000000, -31.99999999999998579 ) ) ;
#12934=CARTESIAN_POINT ( 'NONE',  ( -36.00000000000000711, 6.000000000000000000, -18.00000000000000355 ) ) ;
#12955=DIRECTION ( 'NONE',  ( -0.000000000000000000, 1.000000000000000000, -0.000000000000000000 ) ) ;
#12987=LINE ( 'NONE', #190, #8992 ) ;
#12991=AXIS2_PLACEMENT_3D ( 'NONE', #17329, #4963, #20306 ) ;
#12994=ORIENTED_EDGE ( 'NONE', *, *, #2975, .T. ) ;
#13020=CARTESIAN_POINT ( 'NONE',  ( 22.99999999999998224, 0.000000000000000000, 37.00000000000000711 ) ) ;
#13053=APPLICATION_CONTEXT ( 'automotive_design' ) ;
#13072=ADVANCED_FACE ( 'NONE', ( #2496 ), #14981, .T. ) ;
#13082=DIRECTION ( 'NONE',  ( 0.000000000000000000, 1.000000000000000000, 0.000000000000000000 ) ) ;
#13091=EDGE_LOOP ( 'NONE', ( #8144, #11083, #6318, #5601 ) ) ;
#13100=EDGE_CURVE ( 'NONE', #20017, #11746, #13440, .T. ) ;
#13142=CARTESIAN_POINT ( 'NONE',  ( 36.99999999999999289, 10.00000000000000000, 17.99999999999998934 ) ) ;
#13147=CARTESIAN_POINT ( 'NONE',  ( -32.00000000000000711, 10.00000000000000000, -23.00000000000000000 ) ) ;
#13166=EDGE_CURVE ( 'NONE', #6182, #12416, #9559, .T. ) ;
#13199=ORIENTED_EDGE ( 'NONE', *, *, #16983, .F. ) ;
#13211=CARTESIAN_POINT ( 'NONE',  ( -37.00000000000000711, 0.000000000000000000, 23.00000000000000000 ) ) ;
#13221=ORIENTED_EDGE ( 'NONE', *, *, #11790, .T. ) ;
#13250=DIRECTION ( 'NONE',  ( 0.000000000000000000, 0.000000000000000000, 1.000000000000000000 ) ) ;
#13251=EDGE_LOOP ( 'NONE', ( #15059, #1078, #2826, #19337 ) ) ;
#13260=AXIS2_PLACEMENT_3D ( 'NONE', #15642, #12322, #1674 ) ;
#13261=ORIENTED_EDGE ( 'NONE', *, *, #9880, .F. ) ;
#13277=CARTESIAN_POINT ( 'NONE',  ( -26.00000000000001776, 10.00000000000000000, 31.00000000000003553 ) ) ;
#13305=ADVANCED_FACE ( 'NONE', ( #4252 ), #10532, .T. ) ;
#13308=VECTOR ( 'NONE', #12141, 1000.000000000000000 ) ;
#13317=CARTESIAN_POINT ( 'NONE',  ( 22.99999999999998224, 10.00000000000000000, -31.00000000000003197 ) ) ;
#13318=AXIS2_PLACEMENT_3D ( 'NONE', #19930, #13862, #20131 ) ;
#13328=VECTOR ( 'NONE', #723, 1000.000000000000000 ) ;
#13329=DIRECTION ( 'NONE',  ( -0.000000000000000000, -1.000000000000000000, -0.000000000000000000 ) ) ;
#13331=VECTOR ( 'NONE', #6607, 1000.000000000000000 ) ;
#13333=ORIENTED_EDGE ( 'NONE', *, *, #6771, .F. ) ;
#13336=DIRECTION ( 'NONE',  ( -0.000000000000000000, 1.000000000000000000, -0.000000000000000000 ) ) ;
#13362=ORIENTED_EDGE ( 'NONE', *, *, #9456, .F. ) ;
#13382=ORIENTED_EDGE ( 'NONE', *, *, #1941, .F. ) ;
#13384=PLANE ( 'NONE',  #2674 ) ;
#13391=VECTOR ( 'NONE', #2763, 1000.000000000000000 ) ;
#13401=ORIENTED_EDGE ( 'NONE', *, *, #7954, .T. ) ;
#13415=DIRECTION ( 'NONE',  ( 0.000000000000000000, 1.000000000000000000, 0.000000000000000000 ) ) ;
#13423=EDGE_CURVE ( 'NONE', #6600, #12374, #10085, .T. ) ;
#13434=VERTEX_POINT ( 'NONE', #16091 ) ;
#13439=LINE ( 'NONE', #16738, #5948 ) ;
#13440=LINE ( 'NONE', #19676, #7098 ) ;
#13443=CARTESIAN_POINT ( 'NONE',  ( 31.00000000000001776, 10.00000000000000000, -25.99999999999999645 ) ) ;
#13453=LINE ( 'NONE', #11797, #11184 ) ;
#13475=CARTESIAN_POINT ( 'NONE',  ( 25.99999999999998224, 10.00000000000000000, -31.00000000000003197 ) ) ;
#13477=CARTESIAN_POINT ( 'NONE',  ( 25.99999999999997868, 10.00000000000000000, 40.00000000000000711 ) ) ;
#13482=VECTOR ( 'NONE', #12192, 1000.000000000000000 ) ;
#13507=CARTESIAN_POINT ( 'NONE',  ( 22.99999999999998224, 6.000000000000000000, -36.99999999999999289 ) ) ;
#13511=DIRECTION ( 'NONE',  ( -0.000000000000000000, -0.000000000000000000, 1.000000000000000000 ) ) ;
#13513=ORIENTED_EDGE ( 'NONE', *, *, #1586, .F. ) ;
#13514=CARTESIAN_POINT ( 'NONE',  ( -26.00000000000002132, 10.00000000000000000, -31.00000000000003553 ) ) ;
#13516=ORIENTED_EDGE ( 'NONE', *, *, #5303, .T. ) ;
#13517=AXIS2_PLACEMENT_3D ( 'NONE', #8185, #7024, #5660 ) ;
#13537=CARTESIAN_POINT ( 'NONE',  ( -23.00000000000002132, 0.000000000000000000, 37.00000000000000711 ) ) ;
#13546=CARTESIAN_POINT ( 'NONE',  ( 25.99999999999997868, 0.000000000000000000, 40.00000000000000711 ) ) ;
#13550=VERTEX_POINT ( 'NONE', #7898 ) ;
#13573=CARTESIAN_POINT ( 'NONE',  ( 17.99999999999998579, 10.00000000000000000, -36.99999999999999289 ) ) ;
#13574=EDGE_CURVE ( 'NONE', #15829, #12374, #3043, .T. ) ;
#13579=DIRECTION ( 'NONE',  ( 1.000000000000000000, 0.000000000000000000, 0.000000000000000000 ) ) ;
#13583=ORIENTED_EDGE ( 'NONE', *, *, #18579, .T. ) ;
#13594=DIRECTION ( 'NONE',  ( -3.854941057726255847E-16, -0.000000000000000000, 1.000000000000000000 ) ) ;
#13636=EDGE_CURVE ( 'NONE', #11967, #8401, #14281, .T. ) ;
#13639=AXIS2_PLACEMENT_3D ( 'NONE', #1854, #17637, #3527 ) ;
#13644=DIRECTION ( 'NONE',  ( 0.000000000000000000, 1.000000000000000000, 0.000000000000000000 ) ) ;
#13653=ORIENTED_EDGE ( 'NONE', *, *, #6809, .F. ) ;
#13672=LINE ( 'NONE', #12116, #9775 ) ;
#13681=CARTESIAN_POINT ( 'NONE',  ( 39.99999999999999289, 8.000000000000000000, 18.99999999999999645 ) ) ;
#13691=AXIS2_PLACEMENT_3D ( 'NONE', #10844, #17122, #7187 ) ;
#13705=LINE ( 'NONE', #12458, #13391 ) ;
#13708=PLANE ( 'NONE',  #7178 ) ;
#13718=DIRECTION ( 'NONE',  ( 0.000000000000000000, 0.000000000000000000, -1.000000000000000000 ) ) ;
#13720=ORIENTED_EDGE ( 'NONE', *, *, #440, .F. ) ;
#13723=CARTESIAN_POINT ( 'NONE',  ( -32.00000000000000711, 10.00000000000000000, -22.00000000000000355 ) ) ;
#13731=ORIENTED_EDGE ( 'NONE', *, *, #8300, .F. ) ;
#13739=VERTEX_POINT ( 'NONE', #14665 ) ;
#13742=DIRECTION ( 'NONE',  ( 1.000000000000000000, 0.000000000000000000, 8.673617379884027583E-16 ) ) ;
#13747=EDGE_LOOP ( 'NONE', ( #11631, #10059, #14159, #20071 ) ) ;
#13753=EDGE_CURVE ( 'NONE', #9120, #11912, #1959, .T. ) ;
#13759=DIRECTION ( 'NONE',  ( 0.000000000000000000, 1.000000000000000000, 0.000000000000000000 ) ) ;
#13773=LINE ( 'NONE', #7406, #10860 ) ;
#13779=ORIENTED_EDGE ( 'NONE', *, *, #3969, .T. ) ;
#13783=EDGE_CURVE ( 'NONE', #19948, #17281, #19475, .T. ) ;
#13804=ORIENTED_EDGE ( 'NONE', *, *, #8164, .T. ) ;
#13826=EDGE_CURVE ( 'NONE', #18923, #2094, #16033, .T. ) ;
#13832=ORIENTED_EDGE ( 'NONE', *, *, #14677, .F. ) ;
#13836=DIRECTION ( 'NONE',  ( 0.000000000000000000, 1.000000000000000000, 0.000000000000000000 ) ) ;
#13840=VECTOR ( 'NONE', #12595, 1000.000000000000000 ) ;
#13844=ORIENTED_EDGE ( 'NONE', *, *, #816, .T. ) ;
#13862=DIRECTION ( 'NONE',  ( -1.000000000000000000, 0.000000000000000000, 1.156482317317881191E-15 ) ) ;
#13867=DIRECTION ( 'NONE',  ( 3.854941057726254860E-16, 0.000000000000000000, -1.000000000000000000 ) ) ;
#13873=DIRECTION ( 'NONE',  ( 1.000000000000000000, 0.000000000000000000, -0.000000000000000000 ) ) ;
#13895=CARTESIAN_POINT ( 'NONE',  ( 31.00000000000003553, 10.00000000000000000, -23.00000000000000000 ) ) ;
#13902=VERTEX_POINT ( 'NONE', #5683 ) ;
#13914=CARTESIAN_POINT ( 'NONE',  ( -22.00000000000001776, 8.000000000000000000, 33.00000000000000711 ) ) ;
#13929=CARTESIAN_POINT ( 'NONE',  ( -23.00000000000002132, 10.00000000000000000, 37.00000000000000711 ) ) ;
#13939=FACE_OUTER_BOUND ( 'NONE', #12870, .T. ) ;
#13940=LINE ( 'NONE', #11149, #8241 ) ;
#13955=LINE ( 'NONE', #3233, #2418 ) ;
#13960=CIRCLE ( 'NONE', #9024, 3.000000000000002665 ) ;
#13962=ORIENTED_EDGE ( 'NONE', *, *, #6739, .T. ) ;
#13965=VERTEX_POINT ( 'NONE', #2583 ) ;
#13968=CIRCLE ( 'NONE', #471, 4.000000000000007105 ) ;
#13985=CARTESIAN_POINT ( 'NONE',  ( -31.00000000000005329, 0.000000000000000000, -26.00000000000000355 ) ) ;
#13999=CIRCLE ( 'NONE', #19269, 5.000000000000000888 ) ;
#14012=DIRECTION ( 'NONE',  ( 0.000000000000000000, 0.000000000000000000, -1.000000000000000000 ) ) ;
#14015=EDGE_CURVE ( 'NONE', #6891, #10970, #1308, .T. ) ;
#14016=EDGE_LOOP ( 'NONE', ( #6772, #297, #15881, #5294, #14067, #14909 ) ) ;
#14021=VERTEX_POINT ( 'NONE', #1527 ) ;
#14044=AXIS2_PLACEMENT_3D ( 'NONE', #5955, #18512, #10699 ) ;
#14047=EDGE_CURVE ( 'NONE', #17623, #10970, #5061, .T. ) ;
#14051=EDGE_LOOP ( 'NONE', ( #15135, #3022, #2720, #11241 ) ) ;
#14056=LINE ( 'NONE', #7964, #5109 ) ;
#14061=DIRECTION ( 'NONE',  ( -0.000000000000000000, -1.000000000000000000, 0.000000000000000000 ) ) ;
#14065=EDGE_CURVE ( 'NONE', #5026, #2094, #17324, .T. ) ;
#14067=ORIENTED_EDGE ( 'NONE', *, *, #3078, .F. ) ;
#14086=ADVANCED_FACE ( 'NONE', ( #5990 ), #7637, .F. ) ;
#14087=ORIENTED_EDGE ( 'NONE', *, *, #16140, .F. ) ;
#14088=VERTEX_POINT ( 'NONE', #12387 ) ;
#14113=CARTESIAN_POINT ( 'NONE',  ( -23.00000000000002132, 6.000000000000000000, 32.00000000000000000 ) ) ;
#14142=DIRECTION ( 'NONE',  ( -0.000000000000000000, -1.000000000000000000, -0.000000000000000000 ) ) ;
#14159=ORIENTED_EDGE ( 'NONE', *, *, #19079, .F. ) ;
#14170=DIRECTION ( 'NONE',  ( 0.000000000000000000, -0.000000000000000000, 1.000000000000000000 ) ) ;
#14179=DIRECTION ( 'NONE',  ( 0.000000000000000000, 0.000000000000000000, -1.000000000000000000 ) ) ;
#14193=EDGE_CURVE ( 'NONE', #7139, #17623, #15537, .T. ) ;
#14199=CIRCLE ( 'NONE', #10256, 8.000000000000000000 ) ;
#14206=DIRECTION ( 'NONE',  ( 1.000000000000000000, 0.000000000000000000, 0.000000000000000000 ) ) ;
#14209=VECTOR ( 'NONE', #16069, 1000.000000000000000 ) ;
#14214=ORIENTED_EDGE ( 'NONE', *, *, #5207, .T. ) ;
#14244=FACE_OUTER_BOUND ( 'NONE', #4905, .T. ) ;
#14264=CIRCLE ( 'NONE', #16915, 4.000000000000000000 ) ;
#14268=DIRECTION ( 'NONE',  ( -0.000000000000000000, -1.000000000000000000, -0.000000000000000000 ) ) ;
#14279=LINE ( 'NONE', #19002, #18859 ) ;
#14281=LINE ( 'NONE', #166, #16256 ) ;
#14288=AXIS2_PLACEMENT_3D ( 'NONE', #17044, #18580, #18277 ) ;
#14317=VECTOR ( 'NONE', #20167, 1000.000000000000000 ) ;
#14328=ORIENTED_EDGE ( 'NONE', *, *, #2501, .F. ) ;
#14348=ORIENTED_EDGE ( 'NONE', *, *, #4456, .F. ) ;
#14350=ORIENTED_EDGE ( 'NONE', *, *, #3858, .T. ) ;
#14352=CARTESIAN_POINT ( 'NONE',  ( -23.00000000000002132, 0.000000000000000000, 37.00000000000000711 ) ) ;
#14364=DIRECTION ( 'NONE',  ( -1.000000000000000000, -0.000000000000000000, 3.854941057726247958E-16 ) ) ;
#14367=ORIENTED_EDGE ( 'NONE', *, *, #9487, .T. ) ;
#14383=ORIENTED_EDGE ( 'NONE', *, *, #9890, .F. ) ;
#14385=ADVANCED_FACE ( 'NONE', ( #9132 ), #15426, .F. ) ;
#14392=EDGE_LOOP ( 'NONE', ( #5862, #19946, #3512, #18718 ) ) ;
#14395=ORIENTED_EDGE ( 'NONE', *, *, #5252, .F. ) ;
#14397=LINE ( 'NONE', #9548, #7790 ) ;
#14407=VECTOR ( 'NONE', #9597, 1000.000000000000000 ) ;
#14408=PLANE ( 'NONE',  #11964 ) ;
#14412=CARTESIAN_POINT ( 'NONE',  ( -26.00000000000002132, 8.000000000000000000, 40.00000000000000711 ) ) ;
#14414=DIRECTION ( 'NONE',  ( 1.000000000000000000, 0.000000000000000000, 0.000000000000000000 ) ) ;
#14447=VECTOR ( 'NONE', #19985, 1000.000000000000000 ) ;
#14466=AXIS2_PLACEMENT_3D ( 'NONE', #9996, #1846, #16308 ) ;
#14475=ORIENTED_EDGE ( 'NONE', *, *, #8600, .T. ) ;
#14480=ADVANCED_FACE ( 'NONE', ( #17270 ), #4692, .F. ) ;
#14498=AXIS2_PLACEMENT_3D ( 'NONE', #2245, #14839, #11449 ) ;
#14513=VERTEX_POINT ( 'NONE', #2293 ) ;
#14515=VERTEX_POINT ( 'NONE', #15002 ) ;
#14517=VERTEX_POINT ( 'NONE', #8589 ) ;
#14529=CARTESIAN_POINT ( 'NONE',  ( 39.99999999999999289, 10.00000000000000000, 26.00000000000000000 ) ) ;
#14551=DIRECTION ( 'NONE',  ( 0.000000000000000000, 0.000000000000000000, -1.000000000000000000 ) ) ;
#14575=VERTEX_POINT ( 'NONE', #15302 ) ;
#14589=DIRECTION ( 'NONE',  ( 0.000000000000000000, 0.000000000000000000, 1.000000000000000000 ) ) ;
#14590=VECTOR ( 'NONE', #6694, 1000.000000000000000 ) ;
#14618=DIRECTION ( 'NONE',  ( -0.000000000000000000, 1.000000000000000000, -0.000000000000000000 ) ) ;
#14632=CARTESIAN_POINT ( 'NONE',  ( 25.99999999999997868, 8.000000000000000000, -39.99999999999999289 ) ) ;
#14663=DIRECTION ( 'NONE',  ( 0.000000000000000000, 0.000000000000000000, -1.000000000000000000 ) ) ;
#14665=CARTESIAN_POINT ( 'NONE',  ( 35.99999999999999289, 10.00000000000000000, 18.99999999999999289 ) ) ;
#14667=CARTESIAN_POINT ( 'NONE',  ( 30.99999999999997513, 0.000000000000000000, 30.99999999999999645 ) ) ;
#14677=EDGE_CURVE ( 'NONE', #13902, #15829, #5913, .T. ) ;
#14678=ADVANCED_FACE ( 'NONE', ( #4068 ), #941, .T. ) ;
#14690=CARTESIAN_POINT ( 'NONE',  ( -26.00000000000002132, 8.000000000000000000, 40.00000000000000711 ) ) ;
#14691=CARTESIAN_POINT ( 'NONE',  ( -26.00000000000002132, 0.000000000000000000, -39.99999999999999289 ) ) ;
#14711=DIRECTION ( 'NONE',  ( -0.000000000000000000, 0.000000000000000000, 1.000000000000000000 ) ) ;
#14714=ORIENTED_EDGE ( 'NONE', *, *, #3969, .F. ) ;
#14725=ORIENTED_EDGE ( 'NONE', *, *, #17062, .F. ) ;
#14730=ORIENTED_EDGE ( 'NONE', *, *, #950, .T. ) ;
#14737=LINE ( 'NONE', #17627, #10505 ) ;
#14745=VERTEX_POINT ( 'NONE', #13546 ) ;
#14756=DIRECTION ( 'NONE',  ( -0.000000000000000000, 1.000000000000000000, -0.000000000000000000 ) ) ;
#14759=DIRECTION ( 'NONE',  ( -1.000000000000000000, -0.000000000000000000, -0.000000000000000000 ) ) ;
#14772=ORIENTED_EDGE ( 'NONE', *, *, #6986, .T. ) ;
#14776=CARTESIAN_POINT ( 'NONE',  ( -40.00000000000000711, 8.000000000000000000, -19.00000000000000355 ) ) ;
#14792=EDGE_CURVE ( 'NONE', #1444, #13434, #11048, .T. ) ;
#14800=EDGE_CURVE ( 'NONE', #16197, #7139, #17750, .T. ) ;
#14801=VECTOR ( 'NONE', #16282, 1000.000000000000000 ) ;
#14803=CIRCLE ( 'NONE', #7242, 8.000000000000000000 ) ;
#14818=PRODUCT_DEFINITION_CONTEXT ( 'detailed design', #10922, 'design' ) ;
#14834=AXIS2_PLACEMENT_3D ( 'NONE', #842, #8879, #5805 ) ;
#14839=DIRECTION ( 'NONE',  ( 1.000000000000000000, -0.000000000000000000, 0.000000000000000000 ) ) ;
#14851=ORIENTED_EDGE ( 'NONE', *, *, #642, .T. ) ;
#14854=DIRECTION ( 'NONE',  ( -1.000000000000000000, 0.000000000000000000, 0.000000000000000000 ) ) ;
#14858=CARTESIAN_POINT ( 'NONE',  ( -23.00000000000002487, 10.00000000000000000, -31.00000000000003553 ) ) ;
#14872=VECTOR ( 'NONE', #5102, 1000.000000000000000 ) ;
#14888=DIRECTION ( 'NONE',  ( -0.000000000000000000, -1.000000000000000000, -0.000000000000000000 ) ) ;
#14899=ORIENTED_EDGE ( 'NONE', *, *, #11236, .F. ) ;
#14903=EDGE_LOOP ( 'NONE', ( #8757, #14214, #13731, #1561, #18174, #7597 ) ) ;
#14908=AXIS2_PLACEMENT_3D ( 'NONE', #16584, #2439, #8743 ) ;
#14909=ORIENTED_EDGE ( 'NONE', *, *, #16601, .T. ) ;
#14910=LINE ( 'NONE', #17995, #18585 ) ;
#14913=VECTOR ( 'NONE', #5512, 1000.000000000000000 ) ;
#14934=ORIENTED_EDGE ( 'NONE', *, *, #11079, .F. ) ;
#14957=EDGE_CURVE ( 'NONE', #12424, #10365, #13968, .T. ) ;
#14963=VERTEX_POINT ( 'NONE', #7454 ) ;
#14979=FACE_OUTER_BOUND ( 'NONE', #13251, .T. ) ;
#14981=PLANE ( 'NONE',  #1801 ) ;
#14983=ORIENTED_EDGE ( 'NONE', *, *, #18691, .F. ) ;
#14989=VECTOR ( 'NONE', #9463, 1000.000000000000000 ) ;
#14996=VERTEX_POINT ( 'NONE', #9092 ) ;
#14999=( NAMED_UNIT ( * ) SI_UNIT ( $, .STERADIAN. ) SOLID_ANGLE_UNIT ( ) );
#15002=CARTESIAN_POINT ( 'NONE',  ( 25.99999999999998224, 10.00000000000000000, -32.99999999999999289 ) ) ;
#15016=LINE ( 'NONE', #13475, #5182 ) ;
#15017=ORIENTED_EDGE ( 'NONE', *, *, #14792, .T. ) ;
#15027=( NAMED_UNIT ( * ) SI_UNIT ( $, .STERADIAN. ) SOLID_ANGLE_UNIT ( ) );
#15030=DIRECTION ( 'NONE',  ( -0.000000000000000000, 0.000000000000000000, 1.000000000000000000 ) ) ;
#15053=CARTESIAN_POINT ( 'NONE',  ( -23.00000000000002487, 0.000000000000000000, -31.00000000000003553 ) ) ;
#15055=ORIENTED_EDGE ( 'NONE', *, *, #5226, .F. ) ;
#15059=ORIENTED_EDGE ( 'NONE', *, *, #6809, .T. ) ;
#15062=CARTESIAN_POINT ( 'NONE',  ( -19.00000000000001776, 8.000000000000000000, 40.00000000000000711 ) ) ;
#15066=ADVANCED_FACE ( 'NONE', ( #17634 ), #3523, .F. ) ;
#15082=ORIENTED_EDGE ( 'NONE', *, *, #2318, .F. ) ;
#15085=CARTESIAN_POINT ( 'NONE',  ( -26.00000000000002132, 10.00000000000000000, -39.99999999999999289 ) ) ;
#15097=DIRECTION ( 'NONE',  ( 0.000000000000000000, 1.000000000000000000, 0.000000000000000000 ) ) ;
#15098=ORIENTED_EDGE ( 'NONE', *, *, #12310, .F. ) ;
#15104=ORIENTED_EDGE ( 'NONE', *, *, #8103, .F. ) ;
#15107=CARTESIAN_POINT ( 'NONE',  ( 30.99999999999997513, 10.00000000000000000, 30.99999999999999645 ) ) ;
#15125=DIRECTION ( 'NONE',  ( 0.000000000000000000, 0.000000000000000000, -1.000000000000000000 ) ) ;
#15135=ORIENTED_EDGE ( 'NONE', *, *, #18579, .F. ) ;
#15136=MANIFOLD_SOLID_BREP ( 'Cut-Extrude1', #3059 ) ;
#15142=DIRECTION ( 'NONE',  ( 0.000000000000000000, 0.000000000000000000, -1.000000000000000000 ) ) ;
#15146=AXIS2_PLACEMENT_3D ( 'NONE', #10377, #5634, #7291 ) ;
#15148=ADVANCED_FACE ( 'NONE', ( #8708 ), #5912, .F. ) ;
#15155=ORIENTED_EDGE ( 'NONE', *, *, #13783, .F. ) ;
#15156=CARTESIAN_POINT ( 'NONE',  ( 35.99999999999999289, 8.000000000000000000, 21.99999999999999645 ) ) ;
#15179=EDGE_CURVE ( 'NONE', #1776, #12056, #10362, .T. ) ;
#15210=FACE_OUTER_BOUND ( 'NONE', #5188, .T. ) ;
#15211=PLANE ( 'NONE',  #10660 ) ;
#15217=CARTESIAN_POINT ( 'NONE',  ( -26.00000000000002132, 10.00000000000000000, -31.00000000000003553 ) ) ;
#15228=VECTOR ( 'NONE', #8134, 1000.000000000000000 ) ;
#15231=CARTESIAN_POINT ( 'NONE',  ( -33.00000000000000000, 8.000000000000000000, -22.00000000000000355 ) ) ;
#15233=EDGE_LOOP ( 'NONE', ( #13516, #19784, #9316, #11266, #3215 ) ) ;
#15236=ORIENTED_EDGE ( 'NONE', *, *, #18786, .T. ) ;
#15238=VERTEX_POINT ( 'NONE', #7660 ) ;
#15245=VECTOR ( 'NONE', #10733, 1000.000000000000000 ) ;
#15260=EDGE_LOOP ( 'NONE', ( #15298, #6439, #9856, #2979, #1409, #15580 ) ) ;
#15282=AXIS2_PLACEMENT_3D ( 'NONE', #11161, #238, #131 ) ;
#15288=ORIENTED_EDGE ( 'NONE', *, *, #17534, .T. ) ;
#15298=ORIENTED_EDGE ( 'NONE', *, *, #19949, .F. ) ;
#15302=CARTESIAN_POINT ( 'NONE',  ( 31.00000000000001776, 0.000000000000000000, -25.99999999999999645 ) ) ;
#15314=ORIENTED_EDGE ( 'NONE', *, *, #14677, .T. ) ;
#15327=LINE ( 'NONE', #4201, #11252 ) ;
#15336=CARTESIAN_POINT ( 'NONE',  ( 21.99999999999998224, 10.00000000000000000, -35.99999999999999289 ) ) ;
#15346=EDGE_LOOP ( 'NONE', ( #6123, #14725, #12492, #12994 ) ) ;
#15361=CARTESIAN_POINT ( 'NONE',  ( -23.00000000000002487, 10.00000000000000000, -36.99999999999999289 ) ) ;
#15363=CARTESIAN_POINT ( 'NONE',  ( 25.99999999999998224, 10.00000000000000000, -31.00000000000003197 ) ) ;
#15373=ORIENTED_EDGE ( 'NONE', *, *, #5575, .F. ) ;
#15385=CARTESIAN_POINT ( 'NONE',  ( -22.00000000000001776, 6.000000000000000000, 32.00000000000000711 ) ) ;
#15418=LINE ( 'NONE', #4194, #3483 ) ;
#15421=DIRECTION ( 'NONE',  ( -1.000000000000000000, -0.000000000000000000, 3.854941057726247958E-16 ) ) ;
#15426=PLANE ( 'NONE',  #1807 ) ;
#15432=LINE ( 'NONE', #7695, #9312 ) ;
#15436=DIRECTION ( 'NONE',  ( -0.000000000000000000, -1.000000000000000000, 0.000000000000000000 ) ) ;
#15441=ADVANCED_FACE ( 'NONE', ( #9231 ), #6166, .T. ) ;
#15442=ORIENTED_EDGE ( 'NONE', *, *, #8300, .T. ) ;
#15467=EDGE_CURVE ( 'NONE', #14575, #1752, #13999, .T. ) ;
#15475=VERTEX_POINT ( 'NONE', #12645 ) ;
#15489=ORIENTED_EDGE ( 'NONE', *, *, #19068, .F. ) ;
#15498=VERTEX_POINT ( 'NONE', #1366 ) ;
#15499=DIRECTION ( 'NONE',  ( 0.000000000000000000, -0.000000000000000000, -1.000000000000000000 ) ) ;
#15510=CARTESIAN_POINT ( 'NONE',  ( 17.99999999999998224, 6.000000000000000000, -35.99999999999999289 ) ) ;
#15520=ORIENTED_EDGE ( 'NONE', *, *, #17057, .T. ) ;
#15523=ORIENTED_EDGE ( 'NONE', *, *, #19595, .T. ) ;
#15537=LINE ( 'NONE', #18704, #6037 ) ;
#15542=DIRECTION ( 'NONE',  ( 0.000000000000000000, 0.000000000000000000, 1.000000000000000000 ) ) ;
#15549=VERTEX_POINT ( 'NONE', #9136 ) ;
#15557=EDGE_CURVE ( 'NONE', #8401, #12469, #8570, .T. ) ;
#15561=DIRECTION ( 'NONE',  ( -0.000000000000000000, 0.000000000000000000, 1.000000000000000000 ) ) ;
#15572=CIRCLE ( 'NONE', #13260, 8.000000000000000000 ) ;
#15580=ORIENTED_EDGE ( 'NONE', *, *, #8211, .F. ) ;
#15586=DIRECTION ( 'NONE',  ( 0.000000000000000000, 1.000000000000000000, 0.000000000000000000 ) ) ;
#15590=EDGE_CURVE ( 'NONE', #15549, #865, #15971, .T. ) ;
#15596=LINE ( 'NONE', #9579, #11604 ) ;
#15598=ORIENTED_EDGE ( 'NONE', *, *, #19949, .T. ) ;
#15607=ORIENTED_EDGE ( 'NONE', *, *, #5623, .T. ) ;
#15618=LINE ( 'NONE', #4879, #14407 ) ;
#15626=AXIS2_PLACEMENT_3D ( 'NONE', #9501, #12409, #6433 ) ;
#15628=ORIENTED_EDGE ( 'NONE', *, *, #18698, .T. ) ;
#15634=AXIS2_PLACEMENT_3D ( 'NONE', #10306, #11864, #10416 ) ;
#15635=AXIS2_PLACEMENT_3D ( 'NONE', #19696, #7560, #13742 ) ;
#15642=CARTESIAN_POINT ( 'NONE',  ( -31.00000000000001776, 0.000000000000000000, 31.00000000000000000 ) ) ;
#15643=VECTOR ( 'NONE', #12552, 1000.000000000000000 ) ;
#15690=VECTOR ( 'NONE', #16823, 1000.000000000000000 ) ;
#15741=ADVANCED_FACE ( 'NONE', ( #3419 ), #8884, .T. ) ;
#15760=ORIENTED_EDGE ( 'NONE', *, *, #9046, .T. ) ;
#15766=ORIENTED_EDGE ( 'NONE', *, *, #16058, .F. ) ;
#15778=ORIENTED_EDGE ( 'NONE', *, *, #13636, .F. ) ;
#15815=EDGE_LOOP ( 'NONE', ( #10205, #10659, #7256, #15155 ) ) ;
#15829=VERTEX_POINT ( 'NONE', #9805 ) ;
#15834=VERTEX_POINT ( 'NONE', #9400 ) ;
#15836=CIRCLE ( 'NONE', #6953, 8.000000000000000000 ) ;
#15838=ORIENTED_EDGE ( 'NONE', *, *, #3952, .T. ) ;
#15849=CARTESIAN_POINT ( 'NONE',  ( 21.99999999999998224, 8.000000000000000000, -32.99999999999999289 ) ) ;
#15851=CARTESIAN_POINT ( 'NONE',  ( 25.99999999999998224, 10.00000000000000000, -31.99999999999998579 ) ) ;
#15874=DIRECTION ( 'NONE',  ( -1.000000000000000000, 0.000000000000000000, 0.000000000000000000 ) ) ;
#15881=ORIENTED_EDGE ( 'NONE', *, *, #8750, .T. ) ;
#15892=CARTESIAN_POINT ( 'NONE',  ( 25.99999999999998224, 6.000000000000000000, -31.99999999999998579 ) ) ;
#15914=DIRECTION ( 'NONE',  ( -0.000000000000000000, -1.000000000000000000, -0.000000000000000000 ) ) ;
#15920=DIRECTION ( 'NONE',  ( 0.000000000000000000, 1.000000000000000000, 0.000000000000000000 ) ) ;
#15924=LINE ( 'NONE', #6646, #6299 ) ;
#15925=AXIS2_PLACEMENT_3D ( 'NONE', #20196, #6306, #18960 ) ;
#15945=ADVANCED_FACE ( 'NONE', ( #3828 ), #19658, .F. ) ;
#15953=AXIS2_PLACEMENT_3D ( 'NONE', #18972, #15914, #14663 ) ;
#15971=CIRCLE ( 'NONE', #2420, 5.000000000000000888 ) ;
#15988=CARTESIAN_POINT ( 'NONE',  ( 31.00000000000001421, 10.00000000000000000, 22.99999999999999645 ) ) ;
#15995=CARTESIAN_POINT ( 'NONE',  ( -22.00000000000001776, 8.000000000000000000, 36.00000000000000711 ) ) ;
#15998=LINE ( 'NONE', #20282, #4656 ) ;
#16013=FACE_OUTER_BOUND ( 'NONE', #1384, .T. ) ;
#16016=CARTESIAN_POINT ( 'NONE',  ( -31.00000000000007105, 10.00000000000000000, 23.00000000000000000 ) ) ;
#16029=CARTESIAN_POINT ( 'NONE',  ( -22.00000000000001776, 6.000000000000000000, 32.00000000000000711 ) ) ;
#16033=LINE ( 'NONE', #2264, #12268 ) ;
#16042=CARTESIAN_POINT ( 'NONE',  ( 31.00000000000001421, 0.000000000000000000, 22.99999999999999645 ) ) ;
#16058=EDGE_CURVE ( 'NONE', #11746, #11967, #5754, .T. ) ;
#16059=LINE ( 'NONE', #14691, #16892 ) ;
#16068=ORIENTED_EDGE ( 'NONE', *, *, #6463, .T. ) ;
#16069=DIRECTION ( 'NONE',  ( -4.956352788505164254E-16, 0.000000000000000000, -1.000000000000000000 ) ) ;
#16081=CARTESIAN_POINT ( 'NONE',  ( 30.99999999999997513, 10.00000000000000000, 25.99999999999999645 ) ) ;
#16085=PLANE ( 'NONE',  #4941 ) ;
#16087=EDGE_CURVE ( 'NONE', #865, #13434, #7827, .T. ) ;
#16091=CARTESIAN_POINT ( 'NONE',  ( 30.99999999999997513, 0.000000000000000000, 25.99999999999999645 ) ) ;
#16092=LINE ( 'NONE', #14412, #7877 ) ;
#16093=ORIENTED_EDGE ( 'NONE', *, *, #12681, .F. ) ;
#16117=AXIS2_PLACEMENT_3D ( 'NONE', #731, #10222, #11472 ) ;
#16120=EDGE_LOOP ( 'NONE', ( #16516, #16486, #436, #4313 ) ) ;
#16140=EDGE_CURVE ( 'NONE', #3208, #19115, #18829, .T. ) ;
#16154=ORIENTED_EDGE ( 'NONE', *, *, #11816, .T. ) ;
#16160=CIRCLE ( 'NONE', #15146, 3.000000000000002665 ) ;
#16170=EDGE_CURVE ( 'NONE', #2696, #15549, #4633, .T. ) ;
#16181=VERTEX_POINT ( 'NONE', #6392 ) ;
#16195=VERTEX_POINT ( 'NONE', #3808 ) ;
#16197=VERTEX_POINT ( 'NONE', #5250 ) ;
#16202=CARTESIAN_POINT ( 'NONE',  ( 17.99999999999998224, 10.00000000000000000, -35.99999999999999289 ) ) ;
#16205=DIRECTION ( 'NONE',  ( -0.000000000000000000, -1.000000000000000000, -0.000000000000000000 ) ) ;
#16212=CARTESIAN_POINT ( 'NONE',  ( -23.00000000000002842, 10.00000000000000000, -36.99999999999999289 ) ) ;
#16215=VECTOR ( 'NONE', #7502, 1000.000000000000000 ) ;
#16221=CARTESIAN_POINT ( 'NONE',  ( 31.99999999999998579, 6.000000000000000000, 21.99999999999999645 ) ) ;
#16225=CARTESIAN_POINT ( 'NONE',  ( 36.99999999999999289, 6.000000000000000000, 22.99999999999999645 ) ) ;
#16230=CARTESIAN_POINT ( 'NONE',  ( -22.00000000000001776, 6.000000000000000000, 32.00000000000000711 ) ) ;
#16238=CARTESIAN_POINT ( 'NONE',  ( -33.00000000000000000, 8.000000000000000000, -22.00000000000000355 ) ) ;
#16239=DIRECTION ( 'NONE',  ( 0.000000000000000000, 1.000000000000000000, -0.000000000000000000 ) ) ;
#16246=ORIENTED_EDGE ( 'NONE', *, *, #5479, .F. ) ;
#16248=DIRECTION ( 'NONE',  ( 0.000000000000000000, 1.000000000000000000, -0.000000000000000000 ) ) ;
#16251=EDGE_CURVE ( 'NONE', #10589, #15238, #7204, .T. ) ;
#16256=VECTOR ( 'NONE', #1488, 1000.000000000000000 ) ;
#16275=CARTESIAN_POINT ( 'NONE',  ( -22.00000000000001776, 6.000000000000000000, 36.00000000000000711 ) ) ;
#16282=DIRECTION ( 'NONE',  ( -1.000000000000000000, -0.000000000000000000, -0.000000000000000000 ) ) ;
#16297=AXIS2_PLACEMENT_3D ( 'NONE', #16491, #2345, #8643 ) ;
#16308=DIRECTION ( 'NONE',  ( 0.000000000000000000, 0.000000000000000000, -1.000000000000000000 ) ) ;
#16324=AXIS2_PLACEMENT_3D ( 'NONE', #11966, #2365, #13718 ) ;
#16344=EDGE_CURVE ( 'NONE', #5100, #18923, #9044, .T. ) ;
#16349=EDGE_CURVE ( 'NONE', #4111, #10206, #13773, .T. ) ;
#16366=LINE ( 'NONE', #8492, #10526 ) ;
#16374=ORIENTED_EDGE ( 'NONE', *, *, #19666, .F. ) ;
#16392=FACE_OUTER_BOUND ( 'NONE', #9407, .T. ) ;
#16399=ORIENTED_EDGE ( 'NONE', *, *, #19709, .T. ) ;
#16416=ORIENTED_EDGE ( 'NONE', *, *, #17702, .F. ) ;
#16418=CARTESIAN_POINT ( 'NONE',  ( -22.00000000000001776, 8.000000000000000000, 33.00000000000000711 ) ) ;
#16455=CARTESIAN_POINT ( 'NONE',  ( -33.00000000000000000, 8.000000000000000000, -26.00000000000000355 ) ) ;
#16457=AXIS2_PLACEMENT_3D ( 'NONE', #11799, #13644, #937 ) ;
#16458=CARTESIAN_POINT ( 'NONE',  ( 21.99999999999998224, 6.000000000000000000, -35.99999999999999289 ) ) ;
#16465=ORIENTED_EDGE ( 'NONE', *, *, #7379, .T. ) ;
#16466=LINE ( 'NONE', #1443, #376 ) ;
#16468=ORIENTED_EDGE ( 'NONE', *, *, #8262, .T. ) ;
#16469=EDGE_CURVE ( 'NONE', #15549, #1444, #6790, .T. ) ;
#16474=CARTESIAN_POINT ( 'NONE',  ( -23.00000000000002132, 0.000000000000000000, 37.00000000000000711 ) ) ;
#16486=ORIENTED_EDGE ( 'NONE', *, *, #2707, .F. ) ;
#16491=CARTESIAN_POINT ( 'NONE',  ( 21.99999999999998224, 8.000000000000000000, -35.99999999999999289 ) ) ;
#16493=LINE ( 'NONE', #6824, #4402 ) ;
#16516=ORIENTED_EDGE ( 'NONE', *, *, #8255, .F. ) ;
#16528=LINE ( 'NONE', #11782, #19738 ) ;
#16553=AXIS2_PLACEMENT_3D ( 'NONE', #17373, #7589, #18616 ) ;
#16571=AXIS2_PLACEMENT_3D ( 'NONE', #15336, #18710, #15542 ) ;
#16573=DIRECTION ( 'NONE',  ( 0.000000000000000000, -1.000000000000000000, 0.000000000000000000 ) ) ;
#16574=FACE_OUTER_BOUND ( 'NONE', #9763, .T. ) ;
#16584=CARTESIAN_POINT ( 'NONE',  ( 31.00000000000001421, 10.00000000000000000, 22.99999999999999645 ) ) ;
#16601=EDGE_CURVE ( 'NONE', #17763, #8286, #17394, .T. ) ;
#16612=DIRECTION ( 'NONE',  ( -1.156482317317881191E-15, 0.000000000000000000, -1.000000000000000000 ) ) ;
#16617=CARTESIAN_POINT ( 'NONE',  ( 31.00000000000003553, 10.00000000000000000, -23.00000000000000000 ) ) ;
#16619=FACE_OUTER_BOUND ( 'NONE', #4638, .T. ) ;
#16624=ORIENTED_EDGE ( 'NONE', *, *, #17938, .T. ) ;
#16641=CARTESIAN_POINT ( 'NONE',  ( 35.99999999999999289, 6.000000000000000000, 21.99999999999999645 ) ) ;
#16648=VECTOR ( 'NONE', #10311, 1000.000000000000000 ) ;
#16653=VECTOR ( 'NONE', #10648, 1000.000000000000000 ) ;
#16654=ORIENTED_EDGE ( 'NONE', *, *, #549, .F. ) ;
#16675=CARTESIAN_POINT ( 'NONE',  ( -40.00000000000000711, 10.00000000000000000, -26.00000000000000000 ) ) ;
#16680=ORIENTED_EDGE ( 'NONE', *, *, #13574, .F. ) ;
#16695=DIRECTION ( 'NONE',  ( 1.000000000000000000, 0.000000000000000000, 0.000000000000000000 ) ) ;
#16706=DIRECTION ( 'NONE',  ( -1.000000000000000000, 0.000000000000000000, -0.000000000000000000 ) ) ;
#16717=CARTESIAN_POINT ( 'NONE',  ( -37.00000000000000711, 10.00000000000000000, -18.00000000000000355 ) ) ;
#16725=ORIENTED_EDGE ( 'NONE', *, *, #6239, .T. ) ;
#16731=CARTESIAN_POINT ( 'NONE',  ( -22.00000000000001776, 8.000000000000000000, 36.00000000000000711 ) ) ;
#16733=LINE ( 'NONE', #14858, #13328 ) ;
#16738=CARTESIAN_POINT ( 'NONE',  ( -40.00000000000000711, 10.00000000000000000, 26.00000000000000000 ) ) ;
#16759=ORIENTED_EDGE ( 'NONE', *, *, #4532, .F. ) ;
#16770=DIRECTION ( 'NONE',  ( -0.000000000000000000, -1.000000000000000000, -0.000000000000000000 ) ) ;
#16789=ORIENTED_EDGE ( 'NONE', *, *, #13753, .F. ) ;
#16805=DIRECTION ( 'NONE',  ( -0.000000000000000000, -1.000000000000000000, 0.000000000000000000 ) ) ;
#16808=EDGE_LOOP ( 'NONE', ( #13720, #16759, #3706, #17734, #10938, #235 ) ) ;
#16812=ORIENTED_EDGE ( 'NONE', *, *, #1914, .F. ) ;
#16816=EDGE_CURVE ( 'NONE', #4851, #19516, #15836, .T. ) ;
#16823=DIRECTION ( 'NONE',  ( -0.000000000000000000, -1.000000000000000000, -0.000000000000000000 ) ) ;
#16830=CARTESIAN_POINT ( 'NONE',  ( -18.00000000000001421, 6.000000000000000000, 40.00000000000000711 ) ) ;
#16837=ORIENTED_EDGE ( 'NONE', *, *, #17555, .F. ) ;
#16842=CARTESIAN_POINT ( 'NONE',  ( -33.00000000000000000, 10.00000000000000000, -26.00000000000000355 ) ) ;
#16859=ORIENTED_EDGE ( 'NONE', *, *, #17222, .T. ) ;
#16865=CYLINDRICAL_SURFACE ( 'NONE', #8062, 5.000000000000000888 ) ;
#16891=ADVANCED_FACE ( 'NONE', ( #7868 ), #18780, .T. ) ;
#16892=VECTOR ( 'NONE', #5121, 1000.000000000000000 ) ;
#16894=FACE_OUTER_BOUND ( 'NONE', #9163, .T. ) ;
#16910=VERTEX_POINT ( 'NONE', #12418 ) ;
#16911=EDGE_LOOP ( 'NONE', ( #3730, #12346, #6270, #8292 ) ) ;
#16915=AXIS2_PLACEMENT_3D ( 'NONE', #18589, #10558, #9005 ) ;
#16928=DIRECTION ( 'NONE',  ( -0.000000000000000000, -0.000000000000000000, 1.000000000000000000 ) ) ;
#16930=FACE_OUTER_BOUND ( 'NONE', #13747, .T. ) ;
#16951=EDGE_CURVE ( 'NONE', #14513, #12416, #5097, .T. ) ;
#16960=EDGE_CURVE ( 'NONE', #11944, #11746, #1871, .T. ) ;
#16961=ORIENTED_EDGE ( 'NONE', *, *, #20251, .T. ) ;
#16965=ORIENTED_EDGE ( 'NONE', *, *, #17062, .T. ) ;
#16972=ORIENTED_EDGE ( 'NONE', *, *, #16344, .T. ) ;
#16975=CARTESIAN_POINT ( 'NONE',  ( 31.99999999999998579, 10.00000000000000000, 22.99999999999999645 ) ) ;
#16983=EDGE_CURVE ( 'NONE', #8866, #14996, #15924, .T. ) ;
#16993=EDGE_CURVE ( 'NONE', #18959, #36, #8771, .T. ) ;
#17001=FACE_OUTER_BOUND ( 'NONE', #12903, .T. ) ;
#17005=LINE ( 'NONE', #18638, #19598 ) ;
#17026=DIRECTION ( 'NONE',  ( -1.000000000000000000, -0.000000000000000000, 3.854941057726258312E-16 ) ) ;
#17028=DIRECTION ( 'NONE',  ( -0.000000000000000000, -1.000000000000000000, -0.000000000000000000 ) ) ;
#17042=DIRECTION ( 'NONE',  ( -0.000000000000000000, -1.000000000000000000, 0.000000000000000000 ) ) ;
#17044=CARTESIAN_POINT ( 'NONE',  ( 35.99999999999999289, 6.000000000000000000, 21.99999999999999645 ) ) ;
#17047=VECTOR ( 'NONE', #493, 1000.000000000000000 ) ;
#17052=VERTEX_POINT ( 'NONE', #12826 ) ;
#17054=ORIENTED_EDGE ( 'NONE', *, *, #14015, .F. ) ;
#17057=EDGE_CURVE ( 'NONE', #14021, #6358, #1966, .T. ) ;
#17062=EDGE_CURVE ( 'NONE', #9818, #17052, #19195, .T. ) ;
#17070=CARTESIAN_POINT ( 'NONE',  ( -23.00000000000002487, 0.000000000000000000, -36.99999999999999289 ) ) ;
#17095=EDGE_CURVE ( 'NONE', #16181, #17448, #7617, .T. ) ;
#17107=VECTOR ( 'NONE', #10267, 1000.000000000000000 ) ;
#17111=CARTESIAN_POINT ( 'NONE',  ( -23.00000000000002487, 10.00000000000000000, -31.00000000000003553 ) ) ;
#17122=DIRECTION ( 'NONE',  ( 0.000000000000000000, -1.000000000000000000, 0.000000000000000000 ) ) ;
#17124=ORIENTED_EDGE ( 'NONE', *, *, #17534, .F. ) ;
#17129=FACE_OUTER_BOUND ( 'NONE', #16120, .T. ) ;
#17161=CYLINDRICAL_SURFACE ( 'NONE', #7520, 8.000000000000000000 ) ;
#17195=CARTESIAN_POINT ( 'NONE',  ( 25.99999999999997868, 10.00000000000000000, 40.00000000000000711 ) ) ;
#17203=VECTOR ( 'NONE', #10528, 1000.000000000000000 ) ;
#17222=EDGE_CURVE ( 'NONE', #63, #14745, #15998, .T. ) ;
#17252=CARTESIAN_POINT ( 'NONE',  ( 25.99999999999998224, 10.00000000000000000, -31.00000000000003197 ) ) ;
#17261=EDGE_LOOP ( 'NONE', ( #2309, #3815, #18416, #3906 ) ) ;
#17265=CYLINDRICAL_SURFACE ( 'NONE', #4696, 2.999999999999995559 ) ;
#17268=AXIS2_PLACEMENT_3D ( 'NONE', #4465, #20218, #19999 ) ;
#17270=FACE_OUTER_BOUND ( 'NONE', #10180, .T. ) ;
#17274=DIRECTION ( 'NONE',  ( -0.000000000000000000, -1.000000000000000000, -0.000000000000000000 ) ) ;
#17281=VERTEX_POINT ( 'NONE', #3188 ) ;
#17282=ADVANCED_FACE ( 'NONE', ( #9370 ), #5046, .T. ) ;
#17285=PRODUCT_DEFINITION ( 'UNKNOWN', '', #17850, #14818 ) ;
#17301=PLANE ( 'NONE',  #19188 ) ;
#17307=ORIENTED_EDGE ( 'NONE', *, *, #20216, .T. ) ;
#17319=CARTESIAN_POINT ( 'NONE',  ( -31.00000000000005684, 10.00000000000000000, -23.00000000000000000 ) ) ;
#17324=LINE ( 'NONE', #1738, #18524 ) ;
#17329=CARTESIAN_POINT ( 'NONE',  ( -32.00000000000000711, 6.000000000000000000, -22.00000000000000355 ) ) ;
#17354=SHAPE_REPRESENTATION ( 'Servo-Body.2', ( #2741 ), #3403 ) ;
#17359=EDGE_LOOP ( 'NONE', ( #14348, #14934, #20335, #2317 ) ) ;
#17373=CARTESIAN_POINT ( 'NONE',  ( 31.00000000000003553, 10.00000000000000000, -22.99999999999999645 ) ) ;
#17388=CYLINDRICAL_SURFACE ( 'NONE', #5270, 4.000000000000003553 ) ;
#17394=LINE ( 'NONE', #11114, #8900 ) ;
#17395=CARTESIAN_POINT ( 'NONE',  ( 36.99999999999999289, 10.00000000000000000, 22.99999999999999645 ) ) ;
#17401=AXIS2_PLACEMENT_3D ( 'NONE', #15995, #1916, #2892 ) ;
#17410=CARTESIAN_POINT ( 'NONE',  ( -22.00000000000001776, 8.000000000000000000, 33.00000000000000711 ) ) ;
#17448=VERTEX_POINT ( 'NONE', #4109 ) ;
#17465=DIRECTION ( 'NONE',  ( 0.000000000000000000, -1.000000000000000000, 0.000000000000000000 ) ) ;
#17480=ORIENTED_EDGE ( 'NONE', *, *, #3680, .T. ) ;
#17488=DIRECTION ( 'NONE',  ( -0.000000000000000000, -0.000000000000000000, 1.000000000000000000 ) ) ;
#17509=EDGE_CURVE ( 'NONE', #17448, #18959, #19944, .T. ) ;
#17512=VECTOR ( 'NONE', #20254, 1000.000000000000000 ) ;
#17524=VECTOR ( 'NONE', #19836, 1000.000000000000000 ) ;
#17528=CARTESIAN_POINT ( 'NONE',  ( -40.00000000000000711, 0.000000000000000000, 26.00000000000000000 ) ) ;
#17529=EDGE_LOOP ( 'NONE', ( #2548, #12628, #5186, #6838, #9424 ) ) ;
#17530=CARTESIAN_POINT ( 'NONE',  ( -37.00000000000000711, 0.000000000000000000, 23.00000000000000000 ) ) ;
#17534=EDGE_CURVE ( 'NONE', #18930, #10110, #5758, .T. ) ;
#17547=ORIENTED_EDGE ( 'NONE', *, *, #3216, .T. ) ;
#17554=DIRECTION ( 'NONE',  ( 0.000000000000000000, 0.000000000000000000, -1.000000000000000000 ) ) ;
#17555=EDGE_CURVE ( 'NONE', #15498, #6182, #3262, .T. ) ;
#17559=DIRECTION ( 'NONE',  ( -1.000000000000000000, -0.000000000000000000, -0.000000000000000000 ) ) ;
#17568=VECTOR ( 'NONE', #6128, 1000.000000000000000 ) ;
#17569=LINE ( 'NONE', #12851, #18232 ) ;
#17599=VECTOR ( 'NONE', #12491, 1000.000000000000000 ) ;
#17607=EDGE_CURVE ( 'NONE', #5330, #11362, #18801, .T. ) ;
#17621=CARTESIAN_POINT ( 'NONE',  ( -31.00000000000005329, 0.000000000000000000, 26.00000000000000000 ) ) ;
#17623=VERTEX_POINT ( 'NONE', #19415 ) ;
#17627=CARTESIAN_POINT ( 'NONE',  ( 21.99999999999998224, 6.000000000000000000, -31.99999999999998579 ) ) ;
#17634=FACE_OUTER_BOUND ( 'NONE', #16808, .T. ) ;
#17637=DIRECTION ( 'NONE',  ( -0.000000000000000000, -1.000000000000000000, 0.000000000000000000 ) ) ;
#17641=ORIENTED_EDGE ( 'NONE', *, *, #17095, .F. ) ;
#17670=LINE ( 'NONE', #13147, #9742 ) ;
#17674=LINE ( 'NONE', #14776, #2137 ) ;
#17680=DIRECTION ( 'NONE',  ( 0.000000000000000000, 0.000000000000000000, 1.000000000000000000 ) ) ;
#17681=ORIENTED_EDGE ( 'NONE', *, *, #9691, .T. ) ;
#17691=CIRCLE ( 'NONE', #18984, 3.000000000000002665 ) ;
#17693=EDGE_CURVE ( 'NONE', #10110, #17281, #19131, .T. ) ;
#17702=EDGE_CURVE ( 'NONE', #14088, #9458, #8424, .T. ) ;
#17717=DIRECTION ( 'NONE',  ( 1.000000000000000000, 0.000000000000000000, 0.000000000000000000 ) ) ;
#17720=CARTESIAN_POINT ( 'NONE',  ( -40.00000000000000711, 10.00000000000000000, -19.00000000000000355 ) ) ;
#17727=LINE ( 'NONE', #13211, #18765 ) ;
#17730=DIRECTION ( 'NONE',  ( 0.000000000000000000, 0.000000000000000000, 1.000000000000000000 ) ) ;
#17734=ORIENTED_EDGE ( 'NONE', *, *, #3732, .T. ) ;
#17750=LINE ( 'NONE', #10126, #18872 ) ;
#17763=VERTEX_POINT ( 'NONE', #18377 ) ;
#17782=EDGE_LOOP ( 'NONE', ( #14350, #16961, #11234, #18432, #17480 ) ) ;
#17795=CARTESIAN_POINT ( 'NONE',  ( 31.00000000000003553, 10.00000000000000000, -22.99999999999999645 ) ) ;
#17799=AXIS2_PLACEMENT_3D ( 'NONE', #7669, #18588, #6331 ) ;
#17803=CARTESIAN_POINT ( 'NONE',  ( -31.00000000000002132, 10.00000000000000000, -31.00000000000000000 ) ) ;
#17808=VERTEX_POINT ( 'NONE', #3972 ) ;
#17810=EDGE_CURVE ( 'NONE', #4175, #9239, #10461, .T. ) ;
#17815=LINE ( 'NONE', #16202, #2419 ) ;
#17829=AXIS2_PLACEMENT_3D ( 'NONE', #572, #10064, #8213 ) ;
#17835=LINE ( 'NONE', #2370, #20081 ) ;
#17840=DIRECTION ( 'NONE',  ( -1.000000000000000000, 0.000000000000000000, -1.734723475976807094E-15 ) ) ;
#17850=PRODUCT_DEFINITION_FORMATION_WITH_SPECIFIED_SOURCE ( 'ANY', '', #3169, .NOT_KNOWN. ) ;
#17879=ORIENTED_EDGE ( 'NONE', *, *, #13753, .T. ) ;
#17883=ORIENTED_EDGE ( 'NONE', *, *, #16170, .F. ) ;
#17886=ORIENTED_EDGE ( 'NONE', *, *, #115, .F. ) ;
#17891=PLANE ( 'NONE',  #12676 ) ;
#17906=FACE_OUTER_BOUND ( 'NONE', #8550, .T. ) ;
#17911=EDGE_LOOP ( 'NONE', ( #8493, #17054, #3267, #9961 ) ) ;
#17915=ORIENTED_EDGE ( 'NONE', *, *, #10375, .F. ) ;
#17919=CARTESIAN_POINT ( 'NONE',  ( 35.99999999999999289, 10.00000000000000000, 21.99999999999999645 ) ) ;
#17927=PLANE ( 'NONE',  #4862 ) ;
#17936=EDGE_CURVE ( 'NONE', #20130, #4974, #4887, .T. ) ;
#17938=EDGE_CURVE ( 'NONE', #2920, #1752, #12516, .T. ) ;
#17939=ORIENTED_EDGE ( 'NONE', *, *, #16983, .T. ) ;
#17947=ORIENTED_EDGE ( 'NONE', *, *, #11865, .T. ) ;
#17975=CARTESIAN_POINT ( 'NONE',  ( 22.99999999999998224, 0.000000000000000000, -36.99999999999999289 ) ) ;
#17980=EDGE_LOOP ( 'NONE', ( #18987, #13832, #2913, #10705 ) ) ;
#17983=LINE ( 'NONE', #3876, #3749 ) ;
#17991=VERTEX_POINT ( 'NONE', #6544 ) ;
#17994=VERTEX_POINT ( 'NONE', #9731 ) ;
#17995=CARTESIAN_POINT ( 'NONE',  ( -23.00000000000002132, 6.000000000000000000, 37.00000000000000711 ) ) ;
#18023=CARTESIAN_POINT ( 'NONE',  ( 36.99999999999999289, 0.000000000000000000, -22.99999999999999645 ) ) ;
#18029=EDGE_LOOP ( 'NONE', ( #15766, #7708, #14851, #9552 ) ) ;
#18031=ORIENTED_EDGE ( 'NONE', *, *, #14047, .F. ) ;
#18045=ORIENTED_EDGE ( 'NONE', *, *, #10622, .T. ) ;
#18056=CARTESIAN_POINT ( 'NONE',  ( 39.99999999999999289, 8.000000000000000000, 18.99999999999999645 ) ) ;
#18078=ORIENTED_EDGE ( 'NONE', *, *, #16951, .T. ) ;
#18101=ORIENTED_EDGE ( 'NONE', *, *, #1914, .T. ) ;
#18114=CARTESIAN_POINT ( 'NONE',  ( 22.99999999999998224, 10.00000000000000000, 37.00000000000000711 ) ) ;
#18120=LINE ( 'NONE', #8659, #6751 ) ;
#18130=DIRECTION ( 'NONE',  ( 0.000000000000000000, 1.000000000000000000, 0.000000000000000000 ) ) ;
#18146=ADVANCED_FACE ( 'NONE', ( #3163 ), #9443, .T. ) ;
#18147=ORIENTED_EDGE ( 'NONE', *, *, #17936, .F. ) ;
#18163=CARTESIAN_POINT ( 'NONE',  ( 35.99999999999999289, 6.000000000000000000, 17.99999999999998934 ) ) ;
#18174=ORIENTED_EDGE ( 'NONE', *, *, #6847, .T. ) ;
#18181=FACE_OUTER_BOUND ( 'NONE', #1921, .T. ) ;
#18196=LINE ( 'NONE', #6903, #17047 ) ;
#18223=LINE ( 'NONE', #4135, #12761 ) ;
#18231=ORIENTED_EDGE ( 'NONE', *, *, #5608, .T. ) ;
#18232=VECTOR ( 'NONE', #17680, 1000.000000000000000 ) ;
#18252=AXIS2_PLACEMENT_3D ( 'NONE', #6324, #17042, #12410 ) ;
#18265=ORIENTED_EDGE ( 'NONE', *, *, #5253, .T. ) ;
#18271=ORIENTED_EDGE ( 'NONE', *, *, #1240, .T. ) ;
#18275=LINE ( 'NONE', #8707, #14913 ) ;
#18277=DIRECTION ( 'NONE',  ( 0.000000000000000000, 0.000000000000000000, 1.000000000000000000 ) ) ;
#18283=DIRECTION ( 'NONE',  ( -0.000000000000000000, -1.000000000000000000, 0.000000000000000000 ) ) ;
#18292=ORIENTED_EDGE ( 'NONE', *, *, #17938, .F. ) ;
#18320=CARTESIAN_POINT ( 'NONE',  ( 32.99999999999998579, 8.000000000000000000, 25.99999999999999645 ) ) ;
#18326=PLANE ( 'NONE',  #3141 ) ;
#18337=ORIENTED_EDGE ( 'NONE', *, *, #12710, .T. ) ;
#18339=VECTOR ( 'NONE', #18976, 1000.000000000000000 ) ;
#18377=CARTESIAN_POINT ( 'NONE',  ( -23.00000000000002132, 6.000000000000000000, 37.00000000000000711 ) ) ;
#18407=VECTOR ( 'NONE', #12227, 1000.000000000000000 ) ;
#18416=ORIENTED_EDGE ( 'NONE', *, *, #7414, .F. ) ;
#18426=CIRCLE ( 'NONE', #8547, 3.000000000000002665 ) ;
#18428=DIRECTION ( 'NONE',  ( -0.000000000000000000, -1.000000000000000000, 0.000000000000000000 ) ) ;
#18432=ORIENTED_EDGE ( 'NONE', *, *, #16349, .T. ) ;
#18437=VECTOR ( 'NONE', #9603, 1000.000000000000000 ) ;
#18447=ADVANCED_FACE ( 'NONE', ( #3525 ), #19364, .T. ) ;
#18463=VERTEX_POINT ( 'NONE', #13985 ) ;
#18464=CARTESIAN_POINT ( 'NONE',  ( -32.00000000000000711, 6.000000000000000000, -22.00000000000000355 ) ) ;
#18468=CARTESIAN_POINT ( 'NONE',  ( 32.99999999999998579, 8.000000000000000000, 21.99999999999999645 ) ) ;
#18500=DIRECTION ( 'NONE',  ( 0.000000000000000000, 0.000000000000000000, 1.000000000000000000 ) ) ;
#18512=DIRECTION ( 'NONE',  ( 0.000000000000000000, 0.000000000000000000, 1.000000000000000000 ) ) ;
#18516=LINE ( 'NONE', #7309, #18541 ) ;
#18518=ORIENTED_EDGE ( 'NONE', *, *, #18922, .T. ) ;
#18524=VECTOR ( 'NONE', #17026, 1000.000000000000000 ) ;
#18530=AXIS2_PLACEMENT_3D ( 'NONE', #13914, #5794, #4154 ) ;
#18536=ORIENTED_EDGE ( 'NONE', *, *, #16344, .F. ) ;
#18537=ORIENTED_EDGE ( 'NONE', *, *, #15557, .T. ) ;
#18539=VECTOR ( 'NONE', #1687, 1000.000000000000000 ) ;
#18541=VECTOR ( 'NONE', #13594, 1000.000000000000000 ) ;
#18549=LINE ( 'NONE', #1118, #15245 ) ;
#18566=EDGE_CURVE ( 'NONE', #15475, #2111, #2744, .T. ) ;
#18578=( LENGTH_UNIT ( ) NAMED_UNIT ( * ) SI_UNIT ( .MILLI., .METRE. ) );
#18579=EDGE_CURVE ( 'NONE', #11398, #16195, #10300, .T. ) ;
#18580=DIRECTION ( 'NONE',  ( 0.000000000000000000, 1.000000000000000000, 0.000000000000000000 ) ) ;
#18585=VECTOR ( 'NONE', #14711, 1000.000000000000000 ) ;
#18588=DIRECTION ( 'NONE',  ( 0.000000000000000000, 1.000000000000000000, 0.000000000000000000 ) ) ;
#18589=CARTESIAN_POINT ( 'NONE',  ( -36.00000000000000711, 10.00000000000000000, -22.00000000000000355 ) ) ;
#18603=VECTOR ( 'NONE', #8179, 1000.000000000000000 ) ;
#18612=DIRECTION ( 'NONE',  ( -1.000000000000000000, -0.000000000000000000, -0.000000000000000000 ) ) ;
#18616=DIRECTION ( 'NONE',  ( 1.000000000000000000, 0.000000000000000000, -0.000000000000000000 ) ) ;
#18638=CARTESIAN_POINT ( 'NONE',  ( -37.00000000000000711, 6.000000000000000000, 23.00000000000000000 ) ) ;
#18652=EDGE_LOOP ( 'NONE', ( #6525, #16972, #17681, #4813, #6835 ) ) ;
#18655=DIRECTION ( 'NONE',  ( 0.000000000000000000, -0.000000000000000000, 1.000000000000000000 ) ) ;
#18659=EDGE_CURVE ( 'NONE', #18463, #8369, #15432, .T. ) ;
#18662=ORIENTED_EDGE ( 'NONE', *, *, #13783, .T. ) ;
#18668=ORIENTED_EDGE ( 'NONE', *, *, #16951, .F. ) ;
#18670=DIRECTION ( 'NONE',  ( -0.000000000000000000, -1.000000000000000000, -0.000000000000000000 ) ) ;
#18687=VERTEX_POINT ( 'NONE', #6465 ) ;
#18690=ORIENTED_EDGE ( 'NONE', *, *, #9880, .T. ) ;
#18691=EDGE_CURVE ( 'NONE', #19482, #11967, #4700, .T. ) ;
#18698=EDGE_CURVE ( 'NONE', #3441, #8286, #14279, .T. ) ;
#18700=FACE_OUTER_BOUND ( 'NONE', #17911, .T. ) ;
#18704=CARTESIAN_POINT ( 'NONE',  ( -19.00000000000001776, 8.000000000000000000, 36.00000000000000711 ) ) ;
#18710=DIRECTION ( 'NONE',  ( 0.000000000000000000, 1.000000000000000000, 0.000000000000000000 ) ) ;
#18713=DIRECTION ( 'NONE',  ( -0.000000000000000000, -1.000000000000000000, -0.000000000000000000 ) ) ;
#18718=ORIENTED_EDGE ( 'NONE', *, *, #4532, .T. ) ;
#18722=DIRECTION ( 'NONE',  ( -1.000000000000000000, -0.000000000000000000, -0.000000000000000000 ) ) ;
#18729=DIRECTION ( 'NONE',  ( -1.000000000000000000, -0.000000000000000000, -8.673617379884027583E-16 ) ) ;
#18736=CARTESIAN_POINT ( 'NONE',  ( 30.99999999999997513, 10.00000000000000000, 25.99999999999999645 ) ) ;
#18738=CIRCLE ( 'NONE', #2265, 5.000000000000000888 ) ;
#18765=VECTOR ( 'NONE', #19363, 1000.000000000000000 ) ;
#18780=CYLINDRICAL_SURFACE ( 'NONE', #17799, 4.000000000000000000 ) ;
#18781=EDGE_LOOP ( 'NONE', ( #2281, #10925, #9499, #14367, #3329, #4708 ) ) ;
#18786=EDGE_CURVE ( 'NONE', #72, #16195, #1804, .T. ) ;
#18798=ORIENTED_EDGE ( 'NONE', *, *, #9867, .F. ) ;
#18801=CIRCLE ( 'NONE', #2344, 4.000000000000003553 ) ;
#18814=EDGE_LOOP ( 'NONE', ( #2340, #13333, #13804, #19173 ) ) ;
#18829=LINE ( 'NONE', #20283, #11211 ) ;
#18847=DIRECTION ( 'NONE',  ( 0.000000000000000000, 0.000000000000000000, -1.000000000000000000 ) ) ;
#18859=VECTOR ( 'NONE', #17465, 1000.000000000000000 ) ;
#18869=CARTESIAN_POINT ( 'NONE',  ( 36.99999999999999289, 10.00000000000000000, 22.99999999999999645 ) ) ;
#18872=VECTOR ( 'NONE', #6945, 1000.000000000000000 ) ;
#18891=ORIENTED_EDGE ( 'NONE', *, *, #3732, .F. ) ;
#18895=CARTESIAN_POINT ( 'NONE',  ( 22.99999999999998224, 6.000000000000000000, -31.99999999999998579 ) ) ;
#18900=ORIENTED_EDGE ( 'NONE', *, *, #13574, .T. ) ;
#18922=EDGE_CURVE ( 'NONE', #16181, #17991, #17983, .T. ) ;
#18923=VERTEX_POINT ( 'NONE', #16455 ) ;
#18930=VERTEX_POINT ( 'NONE', #9203 ) ;
#18950=CARTESIAN_POINT ( 'NONE',  ( 35.99999999999999289, 10.00000000000000000, 17.99999999999998934 ) ) ;
#18959=VERTEX_POINT ( 'NONE', #19704 ) ;
#18960=DIRECTION ( 'NONE',  ( 0.000000000000000000, 0.000000000000000000, 1.000000000000000000 ) ) ;
#18962=DIRECTION ( 'NONE',  ( -3.854941057726255847E-16, -0.000000000000000000, 1.000000000000000000 ) ) ;
#18972=CARTESIAN_POINT ( 'NONE',  ( -31.00000000000002132, 10.00000000000000000, -31.00000000000000000 ) ) ;
#18976=DIRECTION ( 'NONE',  ( 0.000000000000000000, 0.000000000000000000, -1.000000000000000000 ) ) ;
#18982=CARTESIAN_POINT ( 'NONE',  ( -26.00000000000002132, 0.000000000000000000, -31.00000000000003553 ) ) ;
#18984=AXIS2_PLACEMENT_3D ( 'NONE', #10105, #13415, #19456 ) ;
#18987=ORIENTED_EDGE ( 'NONE', *, *, #549, .T. ) ;
#18990=DIRECTION ( 'NONE',  ( 0.000000000000000000, 0.000000000000000000, -1.000000000000000000 ) ) ;
#18991=ORIENTED_EDGE ( 'NONE', *, *, #8429, .T. ) ;
#18999=EDGE_CURVE ( 'NONE', #36, #11766, #14264, .T. ) ;
#19002=CARTESIAN_POINT ( 'NONE',  ( -18.00000000000001421, 10.00000000000000000, 37.00000000000000711 ) ) ;
#19006=DIRECTION ( 'NONE',  ( 1.000000000000000000, -0.000000000000000000, 0.000000000000000000 ) ) ;
#19011=DIRECTION ( 'NONE',  ( -0.000000000000000000, -1.000000000000000000, 0.000000000000000000 ) ) ;
#19013=ADVANCED_FACE ( 'NONE', ( #12016 ), #2819, .F. ) ;
#19014=EDGE_LOOP ( 'NONE', ( #936, #1839, #18536, #18231 ) ) ;
#19034=CARTESIAN_POINT ( 'NONE',  ( 25.99999999999998224, 0.000000000000000000, -31.00000000000003197 ) ) ;
#19045=FACE_OUTER_BOUND ( 'NONE', #3754, .T. ) ;
#19047=VECTOR ( 'NONE', #4534, 1000.000000000000000 ) ;
#19052=ADVANCED_FACE ( 'NONE', ( #4674 ), #3139, .F. ) ;
#19055=VECTOR ( 'NONE', #18612, 1000.000000000000000 ) ;
#19058=EDGE_CURVE ( 'NONE', #9818, #4114, #6403, .T. ) ;
#19068=EDGE_CURVE ( 'NONE', #19948, #9269, #13955, .T. ) ;
#19071=VERTEX_POINT ( 'NONE', #18982 ) ;
#19072=LINE ( 'NONE', #17530, #18603 ) ;
#19079=EDGE_CURVE ( 'NONE', #14963, #16910, #8085, .T. ) ;
#19111=CARTESIAN_POINT ( 'NONE',  ( 30.99999999999997513, 10.00000000000000000, 30.99999999999999645 ) ) ;
#19112=LINE ( 'NONE', #15849, #11895 ) ;
#19115=VERTEX_POINT ( 'NONE', #1872 ) ;
#19131=CIRCLE ( 'NONE', #17829, 3.999999999999996447 ) ;
#19142=ORIENTED_EDGE ( 'NONE', *, *, #5575, .T. ) ;
#19152=LINE ( 'NONE', #301, #13331 ) ;
#19159=AXIS2_PLACEMENT_3D ( 'NONE', #19412, #14888, #7075 ) ;
#19173=ORIENTED_EDGE ( 'NONE', *, *, #2707, .T. ) ;
#19184=LINE ( 'NONE', #119, #1138 ) ;
#19188=AXIS2_PLACEMENT_3D ( 'NONE', #1510, #15874, #3184 ) ;
#19195=LINE ( 'NONE', #4989, #12189 ) ;
#19207=ORIENTED_EDGE ( 'NONE', *, *, #16601, .F. ) ;
#19242=VERTEX_POINT ( 'NONE', #8687 ) ;
#19254=VECTOR ( 'NONE', #2297, 1000.000000000000000 ) ;
#19259=CARTESIAN_POINT ( 'NONE',  ( 31.00000000000001421, 10.00000000000000000, 22.99999999999999645 ) ) ;
#19269=AXIS2_PLACEMENT_3D ( 'NONE', #12336, #7697, #14179 ) ;
#19273=CARTESIAN_POINT ( 'NONE',  ( -31.00000000000005329, 10.00000000000000000, -26.00000000000000355 ) ) ;
#19282=DIRECTION ( 'NONE',  ( -0.000000000000000000, 1.000000000000000000, -0.000000000000000000 ) ) ;
#19304=ADVANCED_FACE ( 'NONE', ( #1218 ), #2798, .T. ) ;
#19305=ORIENTED_EDGE ( 'NONE', *, *, #5663, .T. ) ;
#19308=PLANE ( 'NONE',  #7463 ) ;
#19318=VERTEX_POINT ( 'NONE', #3112 ) ;
#19324=EDGE_LOOP ( 'NONE', ( #16789, #16154, #19878, #1187, #344 ) ) ;
#19337=ORIENTED_EDGE ( 'NONE', *, *, #2305, .T. ) ;
#19347=ORIENTED_EDGE ( 'NONE', *, *, #6018, .F. ) ;
#19363=DIRECTION ( 'NONE',  ( 1.000000000000000000, 0.000000000000000000, 0.000000000000000000 ) ) ;
#19364=PLANE ( 'NONE',  #14908 ) ;
#19373=EDGE_CURVE ( 'NONE', #1752, #20152, #20308, .T. ) ;
#19383=CIRCLE ( 'NONE', #17401, 2.999999999999995559 ) ;
#19412=CARTESIAN_POINT ( 'NONE',  ( 30.99999999999997868, 10.00000000000000000, -30.99999999999999645 ) ) ;
#19415=CARTESIAN_POINT ( 'NONE',  ( -19.00000000000001776, 10.00000000000000000, 36.00000000000000711 ) ) ;
#19428=CARTESIAN_POINT ( 'NONE',  ( -23.00000000000002487, 10.00000000000000000, -31.00000000000003553 ) ) ;
#19431=DIRECTION ( 'NONE',  ( 1.000000000000000000, 0.000000000000000000, 0.000000000000000000 ) ) ;
#19434=VECTOR ( 'NONE', #8287, 1000.000000000000000 ) ;
#19456=DIRECTION ( 'NONE',  ( 0.000000000000000000, 0.000000000000000000, 1.000000000000000000 ) ) ;
#19475=LINE ( 'NONE', #16230, #3050 ) ;
#19482=VERTEX_POINT ( 'NONE', #13317 ) ;
#19504=CYLINDRICAL_SURFACE ( 'NONE', #19159, 7.999999999999996447 ) ;
#19510=VECTOR ( 'NONE', #6924, 1000.000000000000000 ) ;
#19516=VERTEX_POINT ( 'NONE', #7029 ) ;
#19518=CARTESIAN_POINT ( 'NONE',  ( 22.99999999999997513, 10.00000000000000000, 31.00000000000005684 ) ) ;
#19534=VECTOR ( 'NONE', #10223, 1000.000000000000000 ) ;
#19562=DIRECTION ( 'NONE',  ( 0.000000000000000000, 1.000000000000000000, 0.000000000000000000 ) ) ;
#19571=EDGE_CURVE ( 'NONE', #17808, #7735, #11674, .T. ) ;
#19577=VERTEX_POINT ( 'NONE', #13020 ) ;
#19592=CARTESIAN_POINT ( 'NONE',  ( 30.99999999999997513, 10.00000000000000000, 30.99999999999999645 ) ) ;
#19595=EDGE_CURVE ( 'NONE', #12469, #11049, #4142, .T. ) ;
#19598=VECTOR ( 'NONE', #15561, 1000.000000000000000 ) ;
#19608=ADVANCED_FACE ( 'NONE', ( #16619 ), #8774, .F. ) ;
#19626=EDGE_CURVE ( 'NONE', #1350, #17623, #18120, .T. ) ;
#19629=LINE ( 'NONE', #3591, #12590 ) ;
#19658=CYLINDRICAL_SURFACE ( 'NONE', #1108, 3.000000000000002665 ) ;
#19666=EDGE_CURVE ( 'NONE', #19577, #17052, #14056, .T. ) ;
#19676=CARTESIAN_POINT ( 'NONE',  ( 31.00000000000003553, 0.000000000000000000, -22.99999999999999645 ) ) ;
#19680=DIRECTION ( 'NONE',  ( 1.000000000000000000, 0.000000000000000000, -3.854941057726247958E-16 ) ) ;
#19681=CARTESIAN_POINT ( 'NONE',  ( -23.00000000000002487, 0.000000000000000000, -36.99999999999999289 ) ) ;
#19693=LINE ( 'NONE', #5414, #4599 ) ;
#19696=CARTESIAN_POINT ( 'NONE',  ( -40.00000000000000711, 8.000000000000000000, -19.00000000000000355 ) ) ;
#19704=CARTESIAN_POINT ( 'NONE',  ( -36.00000000000000711, 6.000000000000000000, -18.00000000000000355 ) ) ;
#19709=EDGE_CURVE ( 'NONE', #14517, #20017, #9598, .T. ) ;
#19724=CARTESIAN_POINT ( 'NONE',  ( -31.00000000000002132, 10.00000000000000000, -31.00000000000000000 ) ) ;
#19738=VECTOR ( 'NONE', #8682, 1000.000000000000000 ) ;
#19740=VECTOR ( 'NONE', #6524, 1000.000000000000000 ) ;
#19748=PLANE ( 'NONE',  #11666 ) ;
#19767=VERTEX_POINT ( 'NONE', #4571 ) ;
#19784=ORIENTED_EDGE ( 'NONE', *, *, #1894, .T. ) ;
#19793=DIRECTION ( 'NONE',  ( -0.000000000000000000, -0.000000000000000000, 1.000000000000000000 ) ) ;
#19829=LINE ( 'NONE', #677, #8239 ) ;
#19836=DIRECTION ( 'NONE',  ( -1.000000000000000000, -0.000000000000000000, -0.000000000000000000 ) ) ;
#19874=( GEOMETRIC_REPRESENTATION_CONTEXT ( 3 ) GLOBAL_UNCERTAINTY_ASSIGNED_CONTEXT ( ( #10113 ) ) GLOBAL_UNIT_ASSIGNED_CONTEXT ( ( #18578, #12292, #14999 ) ) REPRESENTATION_CONTEXT ( 'NONE', 'WORKASPACE' ) );
#19878=ORIENTED_EDGE ( 'NONE', *, *, #17607, .F. ) ;
#19901=EDGE_CURVE ( 'NONE', #16181, #36, #16528, .T. ) ;
#19907=DIRECTION ( 'NONE',  ( -0.000000000000000000, 1.000000000000000000, -0.000000000000000000 ) ) ;
#19918=ORIENTED_EDGE ( 'NONE', *, *, #17222, .F. ) ;
#19929=ADVANCED_FACE ( 'NONE', ( #14979 ), #2495, .F. ) ;
#19930=CARTESIAN_POINT ( 'NONE',  ( 22.99999999999998224, 10.00000000000000000, 37.00000000000000711 ) ) ;
#19931=ORIENTED_EDGE ( 'NONE', *, *, #9222, .F. ) ;
#19937=DIRECTION ( 'NONE',  ( -0.000000000000000000, 1.000000000000000000, -0.000000000000000000 ) ) ;
#19942=LINE ( 'NONE', #9233, #6583 ) ;
#19944=LINE ( 'NONE', #7594, #4328 ) ;
#19946=ORIENTED_EDGE ( 'NONE', *, *, #3467, .F. ) ;
#19948=VERTEX_POINT ( 'NONE', #15385 ) ;
#19949=EDGE_CURVE ( 'NONE', #7815, #3208, #13439, .T. ) ;
#19950=ORIENTED_EDGE ( 'NONE', *, *, #9890, .T. ) ;
#19954=ORIENTED_EDGE ( 'NONE', *, *, #18659, .F. ) ;
#19959=DIRECTION ( 'NONE',  ( 0.000000000000000000, 0.000000000000000000, -1.000000000000000000 ) ) ;
#19975=DIRECTION ( 'NONE',  ( -1.000000000000000000, 0.000000000000000000, 0.000000000000000000 ) ) ;
#19979=PLANE ( 'NONE',  #4822 ) ;
#19980=ADVANCED_FACE ( 'NONE', ( #4014 ), #7130, .T. ) ;
#19985=DIRECTION ( 'NONE',  ( 0.000000000000000000, 0.000000000000000000, -1.000000000000000000 ) ) ;
#19998=ORIENTED_EDGE ( 'NONE', *, *, #17555, .T. ) ;
#19999=DIRECTION ( 'NONE',  ( 0.000000000000000000, 0.000000000000000000, -1.000000000000000000 ) ) ;
#20012=ORIENTED_EDGE ( 'NONE', *, *, #12710, .F. ) ;
#20017=VERTEX_POINT ( 'NONE', #18023 ) ;
#20019=EDGE_LOOP ( 'NONE', ( #16416, #8482, #14383, #16624, #8606, #4921 ) ) ;
#20021=PLANE ( 'NONE',  #13318 ) ;
#20029=CARTESIAN_POINT ( 'NONE',  ( -37.00000000000000711, 10.00000000000000000, -23.00000000000000000 ) ) ;
#20030=AXIS2_PLACEMENT_3D ( 'NONE', #5821, #856, #2288 ) ;
#20034=EDGE_CURVE ( 'NONE', #18959, #20182, #10553, .T. ) ;
#20059=LINE ( 'NONE', #9252, #14317 ) ;
#20071=ORIENTED_EDGE ( 'NONE', *, *, #11443, .T. ) ;
#20081=VECTOR ( 'NONE', #8471, 1000.000000000000000 ) ;
#20094=CARTESIAN_POINT ( 'NONE',  ( 39.99999999999999289, 10.00000000000000000, -26.00000000000000000 ) ) ;
#20121=ORIENTED_EDGE ( 'NONE', *, *, #3532, .F. ) ;
#20130=VERTEX_POINT ( 'NONE', #2865 ) ;
#20131=DIRECTION ( 'NONE',  ( 1.156482317317881191E-15, 0.000000000000000000, 1.000000000000000000 ) ) ;
#20132=CARTESIAN_POINT ( 'NONE',  ( 30.99999999999997868, 10.00000000000000000, -30.99999999999999645 ) ) ;
#20136=DIRECTION ( 'NONE',  ( -0.000000000000000000, -1.000000000000000000, 0.000000000000000000 ) ) ;
#20152=VERTEX_POINT ( 'NONE', #4231 ) ;
#20167=DIRECTION ( 'NONE',  ( 0.000000000000000000, 0.000000000000000000, -1.000000000000000000 ) ) ;
#20182=VERTEX_POINT ( 'NONE', #2964 ) ;
#20186=ORIENTED_EDGE ( 'NONE', *, *, #11662, .T. ) ;
#20196=CARTESIAN_POINT ( 'NONE',  ( -22.00000000000001776, 10.00000000000000000, 36.00000000000000711 ) ) ;
#20200=CARTESIAN_POINT ( 'NONE',  ( -18.00000000000001421, 10.00000000000000000, 40.00000000000000711 ) ) ;
#20212=VERTEX_POINT ( 'NONE', #6188 ) ;
#20214=DIRECTION ( 'NONE',  ( 0.000000000000000000, -1.000000000000000000, 0.000000000000000000 ) ) ;
#20216=EDGE_CURVE ( 'NONE', #17281, #3677, #7614, .T. ) ;
#20218=DIRECTION ( 'NONE',  ( 1.000000000000000000, -0.000000000000000000, 0.000000000000000000 ) ) ;
#20221=ORIENTED_EDGE ( 'NONE', *, *, #16058, .T. ) ;
#20223=CARTESIAN_POINT ( 'NONE',  ( 17.99999999999998224, 6.000000000000000000, -35.99999999999999289 ) ) ;
#20245=ORIENTED_EDGE ( 'NONE', *, *, #3078, .T. ) ;
#20251=EDGE_CURVE ( 'NONE', #13902, #6600, #6081, .T. ) ;
#20254=DIRECTION ( 'NONE',  ( -3.854941057726249437E-16, -0.000000000000000000, 1.000000000000000000 ) ) ;
#20271=CARTESIAN_POINT ( 'NONE',  ( 18.99999999999998224, 10.00000000000000000, -39.99999999999999289 ) ) ;
#20282=CARTESIAN_POINT ( 'NONE',  ( -26.00000000000002132, 0.000000000000000000, 40.00000000000000711 ) ) ;
#20283=CARTESIAN_POINT ( 'NONE',  ( -40.00000000000000711, 10.00000000000000000, 26.00000000000000000 ) ) ;
#20306=DIRECTION ( 'NONE',  ( 0.000000000000000000, 0.000000000000000000, -1.000000000000000000 ) ) ;
#20308=LINE ( 'NONE', #1318, #17599 ) ;
#20316=EDGE_LOOP ( 'NONE', ( #20330, #4520, #8178, #271, #16465 ) ) ;
#20320=ADVANCED_FACE ( 'NONE', ( #1604 ), #17301, .T. ) ;
#20327=DIRECTION ( 'NONE',  ( 0.000000000000000000, 1.000000000000000000, 0.000000000000000000 ) ) ;
#20330=ORIENTED_EDGE ( 'NONE', *, *, #4374, .T. ) ;
#20332=EDGE_CURVE ( 'NONE', #4114, #6573, #12987, .T. ) ;
#20335=ORIENTED_EDGE ( 'NONE', *, *, #1404, .T. ) ;
#20336=EDGE_CURVE ( 'NONE', #9458, #10589, #7920, .T. ) ;
#20339=DIRECTION ( 'NONE',  ( -0.000000000000000000, 1.000000000000000000, -0.000000000000000000 ) ) ;
#20356=ADVANCED_FACE ( 'NONE', ( #4626 ), #14408, .F. ) ;
#20359=ORIENTED_EDGE ( 'NONE', *, *, #8750, .F. ) ;
#20369=DIRECTION ( 'NONE',  ( -0.000000000000000000, -1.000000000000000000, -0.000000000000000000 ) ) ;
ENDSEC;
END-ISO-10303-21;
